ISO-10303-21;
HEADER;
FILE_DESCRIPTION (('STEP AP214'),
    '1' );
FILE_NAME ('hex flange nut_din_Hexagon Flange Nut DIN 6923 - M10 - S.step',
    '2026-10-09T14:04:53',
    ( '' ),
    ( '' ),
    'SwSTEP 2.0',
    'SolidWorks 2021',
    '' );
FILE_SCHEMA (( 'AUTOMOTIVE_DESIGN' ));
ENDSEC;

DATA;
#23=CARTESIAN_POINT ( 'NONE',  ( 0.000000000000000000, 0.000000000000000000, -9.226681596905679683 ) ) ;
#30=DIRECTION ( 'NONE',  ( 0.000000000000000000, 0.000000000000000000, 1.000000000000000000 ) ) ;
#78=B_SPLINE_CURVE_WITH_KNOTS ( 'NONE', 3,
 ( #67643, #99991, #99446, #58484, #91388, #59018, #76777, #77852, #37962, #2880 ),
 .UNSPECIFIED., .F., .F.,
 ( 4, 2, 2, 2, 4 ),
 ( 0.000000000000000000, 0.002305503304226490333, 0.004611006608452981534, 0.006916509912679472301, 0.009222013216905964803 ),
 .UNSPECIFIED. ) ;
#84=CARTESIAN_POINT ( 'NONE',  ( -5.000000000000000000, 0.000000000000000000, -8.553285714285713937 ) ) ;
#86=B_SPLINE_CURVE_WITH_KNOTS ( 'NONE', 3,
 ( #103983, #94324, #70033, #102937, #94862, #53843 ),
 .UNSPECIFIED., .F., .F.,
 ( 4, 2, 4 ),
 ( 2.475503369200647279E-07, 0.002222330217055633675, 0.004444412883774348857 ),
 .UNSPECIFIED. ) ;
#88=ORIENTED_EDGE ( 'NONE', *, *, #84349, .T. ) ;
#186=CARTESIAN_POINT ( 'NONE',  ( -7.500000000000000000, -3.948305025207548002, -7.349903712355482455 ) ) ;
#201=CARTESIAN_POINT ( 'NONE',  ( 0.000000000000000000, 0.000000000000000000, -10.00000000000000000 ) ) ;
#292=CARTESIAN_POINT ( 'NONE',  ( -3.280815508853482498, -7.221948645665456468, -7.591546097228406786 ) ) ;
#359=DIRECTION ( 'NONE',  ( -1.000000000000000000, 0.000000000000000000, 0.000000000000000000 ) ) ;
#439=ORIENTED_EDGE ( 'NONE', *, *, #77485, .F. ) ;
#525=EDGE_CURVE ( 'NONE', #14360, #31711, #89207, .T. ) ;
#548=ORIENTED_EDGE ( 'NONE', *, *, #97150, .F. ) ;
#608=( GEOMETRIC_REPRESENTATION_CONTEXT ( 3 ) GLOBAL_UNCERTAINTY_ASSIGNED_CONTEXT ( ( #68853 ) ) GLOBAL_UNIT_ASSIGNED_CONTEXT ( ( #72048, #79605, #57431 ) ) REPRESENTATION_CONTEXT ( 'NONE', 'WORKASPACE' ) );
#656=FACE_OUTER_BOUND ( 'NONE', #105852, .T. ) ;
#708=CARTESIAN_POINT ( 'NONE',  ( -7.897827455343210623, -1.533134349199915647, -7.633632140068263183 ) ) ;
#774=DIRECTION ( 'NONE',  ( -0.000000000000000000, -0.000000000000000000, -1.000000000000000000 ) ) ;
#784=CIRCLE ( 'NONE', #57622, 5.000000000000000000 ) ;
#823=CARTESIAN_POINT ( 'NONE',  ( -5.274401269815139237, -6.074457022762095093, -7.633824513837116577 ) ) ;
#913=CARTESIAN_POINT ( 'NONE',  ( -5.112021521198779617, 5.708827036477108763, -7.069802615102034338 ) ) ;
#986=LINE ( 'NONE', #79046, #34231 ) ;
#1239=ORIENTED_EDGE ( 'NONE', *, *, #17517, .F. ) ;
#1327=CARTESIAN_POINT ( 'NONE',  ( 2.499999999999999556, -7.216878364870337847, -7.063244554130006847 ) ) ;
#1366=DIRECTION ( 'NONE',  ( -1.000000000000000000, 1.224646799147354686E-16, 0.000000000000000000 ) ) ;
#1411=EDGE_LOOP ( 'NONE', ( #4506, #106407, #66047, #25112 ) ) ;
#1423=DIRECTION ( 'NONE',  ( 0.000000000000000000, 0.000000000000000000, 1.000000000000000000 ) ) ;
#1460=AXIS2_PLACEMENT_3D ( 'NONE', #96325, #38110, #20886 ) ;
#1472=CARTESIAN_POINT ( 'NONE',  ( -7.112481253774054935, 4.553861071371609448, -7.781689322729132385 ) ) ;
#1510=CARTESIAN_POINT ( 'NONE',  ( 0.000000000000000000, 0.000000000000000000, -10.00000000000000000 ) ) ;
#1583=FACE_OUTER_BOUND ( 'NONE', #33137, .T. ) ;
#1631=CARTESIAN_POINT ( 'NONE',  ( 0.000000000000000000, 0.000000000000000000, -0.9215586320570148260 ) ) ;
#1727=FACE_OUTER_BOUND ( 'NONE', #56464, .T. ) ;
#1738=CARTESIAN_POINT ( 'NONE',  ( -6.249999999999997335, 5.051814855409221927, -7.198902722707427593 ) ) ;
#1748=ORIENTED_EDGE ( 'NONE', *, *, #17744, .T. ) ;
#1858=AXIS2_PLACEMENT_3D ( 'NONE', #74347, #24771, #17731 ) ;
#1916=CARTESIAN_POINT ( 'NONE',  ( -6.901579824520443829, 4.675625068323812528, -0.7022220667781287062 ) ) ;
#1956=CARTESIAN_POINT ( 'NONE',  ( 7.922281120364393914, -4.573931137438281169, -8.047472243342934206 ) ) ;
#1960=EDGE_CURVE ( 'NONE', #76808, #81667, #46174, .T. ) ;
#1993=CARTESIAN_POINT ( 'NONE',  ( -5.174575781536625563, -5.672711317432108657, -7.030005583190792606 ) ) ;
#2028=CARTESIAN_POINT ( 'NONE',  ( 7.500000000000000000, -4.330127018922200755, -7.422398894150036064 ) ) ;
#2055=CYLINDRICAL_SURFACE ( 'NONE', #51323, 4.250000000000000000 ) ;
#2136=CARTESIAN_POINT ( 'NONE',  ( -3.288228914120472801, 7.217643567644802971, -7.591235721156638583 ) ) ;
#2160=CARTESIAN_POINT ( 'NONE',  ( -5.000000000000000000, 0.000000000000000000, -4.289342857142857568 ) ) ;
#2168=EDGE_LOOP ( 'NONE', ( #16801, #28743, #105035, #93656 ) ) ;
#2251=CARTESIAN_POINT ( 'NONE',  ( 0.000000000000000000, 0.000000000000000000, -10.00000000000000000 ) ) ;
#2343=VERTEX_POINT ( 'NONE', #8462 ) ;
#2358=CARTESIAN_POINT ( 'NONE',  ( -7.500000000000000888, -1.443375672974072543, -7.063244554130002406 ) ) ;
#2447=DIRECTION ( 'NONE',  ( 1.224646799147353207E-16, 1.000000000000000000, 0.000000000000000000 ) ) ;
#2509=ORIENTED_EDGE ( 'NONE', *, *, #101781, .F. ) ;
#2572=EDGE_CURVE ( 'NONE', #17858, #44884, #47225, .T. ) ;
#2580=EDGE_CURVE ( 'NONE', #66630, #106311, #5686, .T. ) ;
#2788=ORIENTED_EDGE ( 'NONE', *, *, #20568, .F. ) ;
#2858=ORIENTED_EDGE ( 'NONE', *, *, #105350, .T. ) ;
#2860=DIRECTION ( 'NONE',  ( -0.000000000000000000, -0.000000000000000000, -1.000000000000000000 ) ) ;
#2880=CARTESIAN_POINT ( 'NONE',  ( 7.922281120364393914, 4.573931137438267847, -8.047472243342932430 ) ) ;
#3099=CARTESIAN_POINT ( 'NONE',  ( 5.000000000000000000, 6.123233995736766282E-16, -2.868028571428571372 ) ) ;
#3111=AXIS2_PLACEMENT_3D ( 'NONE', #63741, #63204, #39464 ) ;
#3188=DIRECTION ( 'NONE',  ( -0.000000000000000000, -0.000000000000000000, -1.000000000000000000 ) ) ;
#3222=CONICAL_SURFACE ( 'NONE', #92754, 5.000000000000000000, 0.9599310885968913576 ) ;
#3229=ORIENTED_EDGE ( 'NONE', *, *, #89579, .T. ) ;
#3233=LINE ( 'NONE', #37226, #100467 ) ;
#3330=ADVANCED_FACE ( 'NONE', ( #103467 ), #29616, .T. ) ;
#3351=VECTOR ( 'NONE', #73625, 1000.000000000000000 ) ;
#3384=EDGE_LOOP ( 'NONE', ( #61050, #90181, #23921, #56561 ) ) ;
#3386=DIRECTION ( 'NONE',  ( 0.000000000000000000, 0.000000000000000000, 1.000000000000000000 ) ) ;
#3424=CARTESIAN_POINT ( 'NONE',  ( 3.750000000000004885, -6.495190528383287365, 1.734723475976807094E-15 ) ) ;
#3518=DIRECTION ( 'NONE',  ( -0.000000000000000000, -0.000000000000000000, 1.000000000000000000 ) ) ;
#3547=ORIENTED_EDGE ( 'NONE', *, *, #45819, .T. ) ;
#3608=EDGE_CURVE ( 'NONE', #10075, #96318, #85505, .T. ) ;
#3661=EDGE_LOOP ( 'NONE', ( #78997, #21671, #2858, #102892 ) ) ;
#3671=EDGE_CURVE ( 'NONE', #27490, #60305, #35765, .T. ) ;
#3700=ORIENTED_EDGE ( 'NONE', *, *, #81380, .T. ) ;
#3730=EDGE_CURVE ( 'NONE', #2343, #72931, #89073, .T. ) ;
#3733=CARTESIAN_POINT ( 'NONE',  ( 0.000000000000000000, 0.000000000000000000, -8.553285714285713937 ) ) ;
#3745=CARTESIAN_POINT ( 'NONE',  ( -7.500000000000000000, 4.330127018922188320, -0.9999999999999904521 ) ) ;
#3978=VECTOR ( 'NONE', #63858, 1000.000000000000000 ) ;
#4046=DIRECTION ( 'NONE',  ( 0.000000000000000000, 0.000000000000000000, 1.000000000000000000 ) ) ;
#4047=AXIS2_PLACEMENT_3D ( 'NONE', #84903, #82769, #59576 ) ;
#4153=VERTEX_POINT ( 'NONE', #64670 ) ;
#4170=DIRECTION ( 'NONE',  ( -0.000000000000000000, -0.000000000000000000, -1.000000000000000000 ) ) ;
#4184=CARTESIAN_POINT ( 'NONE',  ( 0.000000000000000000, 0.000000000000000000, -0.9215586320570148260 ) ) ;
#4256=CARTESIAN_POINT ( 'NONE',  ( 0.000000000000000000, 0.000000000000000000, -3.764187203485586330 ) ) ;
#4320=ADVANCED_FACE ( 'NONE', ( #101296 ), #90927, .F. ) ;
#4357=DIRECTION ( 'NONE',  ( -0.000000000000000000, -0.000000000000000000, -1.000000000000000000 ) ) ;
#4416=VERTEX_POINT ( 'NONE', #103931 ) ;
#4439=FACE_OUTER_BOUND ( 'NONE', #3661, .T. ) ;
#4461=EDGE_LOOP ( 'NONE', ( #44124, #96132, #37187, #39749 ) ) ;
#4475=CARTESIAN_POINT ( 'NONE',  ( -5.000000000000000000, 0.000000000000000000, -0.02540000000000007530 ) ) ;
#4506=ORIENTED_EDGE ( 'NONE', *, *, #103491, .F. ) ;
#4667=CIRCLE ( 'NONE', #20259, 7.500000000000003553 ) ;
#4678=EDGE_CURVE ( 'NONE', #75707, #32369, #36871, .T. ) ;
#4762=EDGE_LOOP ( 'NONE', ( #15905, #3229, #36012, #49748 ) ) ;
#4837=EDGE_CURVE ( 'NONE', #73538, #100365, #41978, .T. ) ;
#4897=CARTESIAN_POINT ( 'NONE',  ( 0.000000000000000000, 0.000000000000000000, -0.02540000000000007530 ) ) ;
#4899=VECTOR ( 'NONE', #72016, 1000.000000000000000 ) ;
#4925=CIRCLE ( 'NONE', #8368, 4.250000000000000000 ) ;
#4966=CLOSED_SHELL ( 'NONE', ( #64446, #104900, #55999, #10950, #60829, #69337, #80858, #83078, #49138, #89734, #34147, #92399, #14468, #69279, #22941, #4320, #77794, #31123, #56221, #47110, #41508, #12104, #94571, #103164, #98553, #98155, #102612, #63890, #56626, #63187, #27152, #14239, #75832, #31602, #54738, #92628, #3330, #32117, #26082, #95568, #7639, #72400, #56809, #68174, #48973, #77109, #12866, #6197, #88799, #13340, #71181, #27520, #43912, #6079, #40802, #23803, #88156, #25061, #73906, #73592, #57109, #17146, #32240, #67446, #35718, #70666, #89674, #97498, #103747, #76630, #23436, #23546 ) ) ;
#4981=ORIENTED_EDGE ( 'NONE', *, *, #75906, .T. ) ;
#5121=CARTESIAN_POINT ( 'NONE',  ( -2.452879891156814374, -7.244083172395190395, -0.1007566405101844587 ) ) ;
#5157=ORIENTED_EDGE ( 'NONE', *, *, #103851, .F. ) ;
#5162=DIRECTION ( 'NONE',  ( 1.000000000000000000, 0.000000000000000000, 0.000000000000000000 ) ) ;
#5168=CARTESIAN_POINT ( 'NONE',  ( 7.500000000000001776, -2.571118828324945760, -0.3627527587569074341 ) ) ;
#5227=FACE_OUTER_BOUND ( 'NONE', #50890, .T. ) ;
#5299=ORIENTED_EDGE ( 'NONE', *, *, #85732, .F. ) ;
#5306=CARTESIAN_POINT ( 'NONE',  ( 0.000000000000000000, 0.000000000000000000, 0.000000000000000000 ) ) ;
#5316=CARTESIAN_POINT ( 'NONE',  ( 7.500000000000000000, 4.330127018922189208, -7.422398894150033399 ) ) ;
#5371=AXIS2_PLACEMENT_3D ( 'NONE', #25603, #9350, #40672 ) ;
#5416=CARTESIAN_POINT ( 'NONE',  ( 0.000000000000000000, 0.000000000000000000, -3.393184225085859929 ) ) ;
#5654=CARTESIAN_POINT ( 'NONE',  ( 7.500000000000000888, 0.3744244963005072258, 2.475665546587506316E-15 ) ) ;
#5686=LINE ( 'NONE', #87685, #4899 ) ;
#5772=CIRCLE ( 'NONE', #41958, 4.250000000000000000 ) ;
#5828=CARTESIAN_POINT ( 'NONE',  ( 7.500000000000001776, 4.330127018922189208, -7.564338275809342704 ) ) ;
#5894=VECTOR ( 'NONE', #102528, 1000.000000000000000 ) ;
#5909=VECTOR ( 'NONE', #33520, 1000.000000000000000 ) ;
#5978=EDGE_CURVE ( 'NONE', #100365, #96318, #27697, .T. ) ;
#5997=CARTESIAN_POINT ( 'NONE',  ( 7.500000000000000000, -1.645076096009009836, -7.030022527230193496 ) ) ;
#6063=ORIENTED_EDGE ( 'NONE', *, *, #88792, .T. ) ;
#6074=AXIS2_PLACEMENT_3D ( 'NONE', #39483, #32992, #6548 ) ;
#6079=ADVANCED_FACE ( 'NONE', ( #65702 ), #75393, .F. ) ;
#6147=ORIENTED_EDGE ( 'NONE', *, *, #103336, .F. ) ;
#6197=ADVANCED_FACE ( 'NONE', ( #59749 ), #63618, .T. ) ;
#6280=EDGE_CURVE ( 'NONE', #38530, #34113, #36478, .T. ) ;
#6336=CARTESIAN_POINT ( 'NONE',  ( 0.000000000000000000, 0.000000000000000000, -8.500000000000000000 ) ) ;
#6403=CARTESIAN_POINT ( 'NONE',  ( 5.147825380265281581, 5.688155668807426402, -7.450218641349906079 ) ) ;
#6427=CIRCLE ( 'NONE', #46113, 0.7733184030943203169 ) ;
#6548=DIRECTION ( 'NONE',  ( -1.000000000000000000, 0.000000000000000000, 0.000000000000000000 ) ) ;
#6584=EDGE_CURVE ( 'NONE', #29730, #34186, #17185, .T. ) ;
#6602=CARTESIAN_POINT ( 'NONE',  ( -4.250000000000000000, 5.204748896376250699E-16, -3.393184225085859929 ) ) ;
#6623=DIRECTION ( 'NONE',  ( -0.000000000000000000, -0.000000000000000000, -1.000000000000000000 ) ) ;
#6651=ORIENTED_EDGE ( 'NONE', *, *, #63592, .F. ) ;
#6673=CONICAL_SURFACE ( 'NONE', #13525, 5.000000000000000000, 0.9599310885968913576 ) ;
#6723=CARTESIAN_POINT ( 'NONE',  ( -7.915341292092665348, -3.857523022641996757, -7.913710289178197854 ) ) ;
#6753=DIRECTION ( 'NONE',  ( -0.000000000000000000, -0.000000000000000000, 1.000000000000000000 ) ) ;
#6774=CARTESIAN_POINT ( 'NONE',  ( 3.750000000000007105, 6.495190528383288253, 1.734723475976807094E-15 ) ) ;
#6836=DIRECTION ( 'NONE',  ( -0.8191520442889913545, 0.000000000000000000, -0.5735764363510468256 ) ) ;
#6940=ORIENTED_EDGE ( 'NONE', *, *, #62106, .F. ) ;
#6941=EDGE_CURVE ( 'NONE', #32369, #18346, #40235, .T. ) ;
#6951=CARTESIAN_POINT ( 'NONE',  ( 0.000000000000000000, 0.000000000000000000, -9.974599999999998801 ) ) ;
#6984=CARTESIAN_POINT ( 'NONE',  ( 4.250000000000000000, 0.000000000000000000, -2.342872917771300578 ) ) ;
#7086=EDGE_LOOP ( 'NONE', ( #2788, #40416, #106431 ) ) ;
#7242=CARTESIAN_POINT ( 'NONE',  ( -7.500000000000000000, 1.644753667992016055, -7.029983668656049289 ) ) ;
#7313=CARTESIAN_POINT ( 'NONE',  ( 4.250000000000000000, 0.000000000000000000, -6.235812796514431433 ) ) ;
#7490=SHAPE_REPRESENTATION ( 'hex flange nut_din_Hexagon Flange Nut DIN 6923 - M10 - S', ( #10728 ), #71253 ) ;
#7530=EDGE_CURVE ( 'NONE', #24961, #31711, #100596, .T. ) ;
#7639=ADVANCED_FACE ( 'NONE', ( #38031, #103782 ), #63879, .T. ) ;
#7773=CARTESIAN_POINT ( 'NONE',  ( -7.500000000000000000, -0.7729939684968888391, -7.026407045654482708 ) ) ;
#7858=DIRECTION ( 'NONE',  ( -0.000000000000000000, -0.000000000000000000, -1.000000000000000000 ) ) ;
#7915=VECTOR ( 'NONE', #23048, 1000.000000000000000 ) ;
#7926=CARTESIAN_POINT ( 'NONE',  ( 2.500000000000000000, 7.216878364870322748, -7.063244554130003294 ) ) ;
#7962=ORIENTED_EDGE ( 'NONE', *, *, #38290, .T. ) ;
#8004=DIRECTION ( 'NONE',  ( -1.000000000000000000, 0.000000000000000000, 0.000000000000000000 ) ) ;
#8047=LINE ( 'NONE', #80875, #92775 ) ;
#8113=CARTESIAN_POINT ( 'NONE',  ( -6.318250223874061420E-16, 9.147862274876551680, -8.047472243342934206 ) ) ;
#8118=CARTESIAN_POINT ( 'NONE',  ( 7.499999999999999112, 4.652409454067512051, -7.929128589908465585 ) ) ;
#8121=CARTESIAN_POINT ( 'NONE',  ( 4.981862520314373377, 0.000000000000000000, -0.01270000000000090501 ) ) ;
#8165=ORIENTED_EDGE ( 'NONE', *, *, #77851, .F. ) ;
#8272=EDGE_LOOP ( 'NONE', ( #72872, #75943, #27788, #39354 ) ) ;
#8308=CARTESIAN_POINT ( 'NONE',  ( 4.250000000000000000, 0.000000000000000000, -9.449444346342716017 ) ) ;
#8367=CARTESIAN_POINT ( 'NONE',  ( 0.000000000000000000, 0.000000000000000000, -9.449444346342716017 ) ) ;
#8368=AXIS2_PLACEMENT_3D ( 'NONE', #50334, #48734, #74609 ) ;
#8462=CARTESIAN_POINT ( 'NONE',  ( 4.250000000000000000, 0.000000000000000000, -0.9215586320570148260 ) ) ;
#8478=DIRECTION ( 'NONE',  ( 0.000000000000000000, 0.000000000000000000, 1.000000000000000000 ) ) ;
#8515=FACE_OUTER_BOUND ( 'NONE', #34719, .T. ) ;
#8559=CARTESIAN_POINT ( 'NONE',  ( 0.000000000000000000, 0.000000000000000000, -6.235812796514431433 ) ) ;
#8619=CARTESIAN_POINT ( 'NONE',  ( -1.250000000000000222, -7.938566201357373231, -7.198902722707432922 ) ) ;
#8652=CARTESIAN_POINT ( 'NONE',  ( 7.499999999999999112, 3.105728215500127565, -7.659336188854855898 ) ) ;
#8713=CARTESIAN_POINT ( 'NONE',  ( -7.922281120364393914, -4.573931137438282057, -8.047472243342934206 ) ) ;
#8734=CARTESIAN_POINT ( 'NONE',  ( -4.250000000000000000, 5.204748896376250699E-16, -7.657127082228716297 ) ) ;
#8776=DIRECTION ( 'NONE',  ( -1.000000000000000000, 0.000000000000000000, 0.000000000000000000 ) ) ;
#8831=ORIENTED_EDGE ( 'NONE', *, *, #87345, .F. ) ;
#8919=CARTESIAN_POINT ( 'NONE',  ( -7.500000000000000000, -1.486698507076798847, -0.09861472150523799274 ) ) ;
#8923=DIRECTION ( 'NONE',  ( -1.000000000000000000, 0.000000000000000000, 0.000000000000000000 ) ) ;
#8972=EDGE_CURVE ( 'NONE', #103169, #11929, #83920, .T. ) ;
#9095=DIRECTION ( 'NONE',  ( -0.000000000000000000, -0.000000000000000000, 1.000000000000000000 ) ) ;
#9115=AXIS2_PLACEMENT_3D ( 'NONE', #48798, #81689, #73610 ) ;
#9141=CARTESIAN_POINT ( 'NONE',  ( -5.000000000000000000, 0.000000000000000000, -2.868028571428571372 ) ) ;
#9155=LINE ( 'NONE', #99772, #82033 ) ;
#9161=FACE_OUTER_BOUND ( 'NONE', #99135, .T. ) ;
#9189=CARTESIAN_POINT ( 'NONE',  ( -1.843253007570911225E-16, -9.147862274876562338, -8.047472243342939535 ) ) ;
#9325=EDGE_CURVE ( 'NONE', #30487, #10693, #78, .T. ) ;
#9350=DIRECTION ( 'NONE',  ( -1.000000000000000000, 0.000000000000000000, 0.000000000000000000 ) ) ;
#9383=VERTEX_POINT ( 'NONE', #102659 ) ;
#9411=DIRECTION ( 'NONE',  ( -0.000000000000000000, -0.000000000000000000, -1.000000000000000000 ) ) ;
#9514=CARTESIAN_POINT ( 'NONE',  ( 0.6249999999999998890, 8.299410119600874935, -7.298562697733109061 ) ) ;
#9675=CONICAL_SURFACE ( 'NONE', #16548, 5.000000000000000000, 0.9599310885968913576 ) ;
#9701=CARTESIAN_POINT ( 'NONE',  ( -1.305263714129178521, 8.377797850839289850, -7.792447862505335721 ) ) ;
#9719=DIRECTION ( 'NONE',  ( -1.000000000000000000, 0.000000000000000000, 0.000000000000000000 ) ) ;
#9763=CARTESIAN_POINT ( 'NONE',  ( -5.000000000000000000, 6.123233995736766282E-16, 0.000000000000000000 ) ) ;
#9823=AXIS2_PLACEMENT_3D ( 'NONE', #69723, #102615, #45978 ) ;
#9824=CARTESIAN_POINT ( 'NONE',  ( 0.000000000000000000, 0.000000000000000000, -10.00000000000000000 ) ) ;
#9885=EDGE_CURVE ( 'NONE', #32589, #45380, #101738, .T. ) ;
#9950=EDGE_LOOP ( 'NONE', ( #91534, #46239, #50910, #99790 ) ) ;
#9990=ORIENTED_EDGE ( 'NONE', *, *, #69469, .F. ) ;
#10070=AXIS2_PLACEMENT_3D ( 'NONE', #10676, #101308, #43592 ) ;
#10075=VERTEX_POINT ( 'NONE', #87162 ) ;
#10114=CARTESIAN_POINT ( 'NONE',  ( -7.169303301815157958, 4.521054846639327884, -7.349897473155612815 ) ) ;
#10148=ORIENTED_EDGE ( 'NONE', *, *, #77919, .T. ) ;
#10155=FACE_OUTER_BOUND ( 'NONE', #89397, .T. ) ;
#10184=ORIENTED_EDGE ( 'NONE', *, *, #78866, .F. ) ;
#10191=ORIENTED_EDGE ( 'NONE', *, *, #23188, .F. ) ;
#10247=EDGE_LOOP ( 'NONE', ( #19828, #43654, #31346, #8831 ) ) ;
#10310=AXIS2_PLACEMENT_3D ( 'NONE', #52551, #42877, #10503 ) ;
#10314=AXIS2_PLACEMENT_3D ( 'NONE', #82414, #100189, #42480 ) ;
#10439=VECTOR ( 'NONE', #36823, 1000.000000000000000 ) ;
#10441=ORIENTED_EDGE ( 'NONE', *, *, #1960, .F. ) ;
#10503=DIRECTION ( 'NONE',  ( -1.000000000000000000, 0.000000000000000000, 0.000000000000000000 ) ) ;
#10507=CARTESIAN_POINT ( 'NONE',  ( 0.6250000000000004441, -8.299410119600883817, -7.298562697733114391 ) ) ;
#10627=CARTESIAN_POINT ( 'NONE',  ( -7.500000000000005329, 4.330127018922183879, -7.564335161054492218 ) ) ;
#10641=LINE ( 'NONE', #3099, #49404 ) ;
#10676=CARTESIAN_POINT ( 'NONE',  ( 0.000000000000000000, 0.000000000000000000, -10.00000000000000000 ) ) ;
#10693=VERTEX_POINT ( 'NONE', #64862 ) ;
#10727=DIRECTION ( 'NONE',  ( -0.000000000000000000, -0.000000000000000000, 1.000000000000000000 ) ) ;
#10728=AXIS2_PLACEMENT_3D ( 'NONE', #14983, #57033, #47878 ) ;
#10780=CARTESIAN_POINT ( 'NONE',  ( 5.276765049035075705, -6.073111908730308706, -7.634085501268430107 ) ) ;
#10797=DIRECTION ( 'NONE',  ( -1.000000000000000000, 0.000000000000000000, 0.000000000000000000 ) ) ;
#10847=AXIS2_PLACEMENT_3D ( 'NONE', #58286, #35113, #9719 ) ;
#10851=FACE_OUTER_BOUND ( 'NONE', #20186, .T. ) ;
#10938=CARTESIAN_POINT ( 'NONE',  ( 0.000000000000000000, 0.000000000000000000, -8.028130060628445364 ) ) ;
#10950=ADVANCED_FACE ( 'NONE', ( #102548 ), #61392, .F. ) ;
#10954=( GEOMETRIC_REPRESENTATION_CONTEXT ( 3 ) GLOBAL_UNCERTAINTY_ASSIGNED_CONTEXT ( ( #59673 ) ) GLOBAL_UNIT_ASSIGNED_CONTEXT ( ( #87462, #68634, #46975 ) ) REPRESENTATION_CONTEXT ( 'NONE', 'WORKASPACE' ) );
#11012=ORIENTED_EDGE ( 'NONE', *, *, #25006, .F. ) ;
#11142=CARTESIAN_POINT ( 'NONE',  ( -5.000000000000000000, 0.000000000000000000, -5.710657142857142432 ) ) ;
#11262=DIRECTION ( 'NONE',  ( 0.8191520442889975717, 1.003171929053531773E-16, -0.5735764363510378328 ) ) ;
#11405=DIRECTION ( 'NONE',  ( -1.000000000000000000, 0.000000000000000000, 0.000000000000000000 ) ) ;
#11921=CARTESIAN_POINT ( 'NONE',  ( 7.500000000000000888, 1.443375672974059443, -7.063244554130002406 ) ) ;
#11929=VERTEX_POINT ( 'NONE', #66699 ) ;
#12016=DIRECTION ( 'NONE',  ( -0.000000000000000000, -0.000000000000000000, -1.000000000000000000 ) ) ;
#12104=ADVANCED_FACE ( 'NONE', ( #74115 ), #32096, .F. ) ;
#12140=DIRECTION ( 'NONE',  ( -0.8191520442889975717, 0.000000000000000000, -0.5735764363510378328 ) ) ;
#12244=AXIS2_PLACEMENT_3D ( 'NONE', #64403, #22897, #62811 ) ;
#12273=DIRECTION ( 'NONE',  ( -1.000000000000000000, 0.000000000000000000, 0.000000000000000000 ) ) ;
#12307=EDGE_LOOP ( 'NONE', ( #55933, #69282, #62589, #105063, #58848, #86126, #88679 ) ) ;
#12367=CARTESIAN_POINT ( 'NONE',  ( 0.000000000000000000, 0.000000000000000000, -0.5505556536572887572 ) ) ;
#12410=VERTEX_POINT ( 'NONE', #18037 ) ;
#12467=CARTESIAN_POINT ( 'NONE',  ( 4.250000000000000000, 0.000000000000000000, -5.185501489199872083 ) ) ;
#12489=CARTESIAN_POINT ( 'NONE',  ( -4.250000000000000000, 5.204748896376250699E-16, -10.00000000000000000 ) ) ;
#12551=DIRECTION ( 'NONE',  ( -0.8191520442889884679, 1.003171929053520679E-16, 0.5735764363510508224 ) ) ;
#12733=VECTOR ( 'NONE', #57975, 1000.000000000000000 ) ;
#12866=ADVANCED_FACE ( 'NONE', ( #22168 ), #14864, .T. ) ;
#12899=CARTESIAN_POINT ( 'NONE',  ( 7.968863443239238009, 4.547634245050472757, -8.057411785091789014 ) ) ;
#12999=ORIENTED_EDGE ( 'NONE', *, *, #20568, .T. ) ;
#13085=LINE ( 'NONE', #87536, #18045 ) ;
#13149=ORIENTED_EDGE ( 'NONE', *, *, #56286, .T. ) ;
#13261=ORIENTED_EDGE ( 'NONE', *, *, #17533, .T. ) ;
#13263=VECTOR ( 'NONE', #94061, 1000.000000000000000 ) ;
#13340=ADVANCED_FACE ( 'NONE', ( #92072 ), #89888, .F. ) ;
#13350=VERTEX_POINT ( 'NONE', #101245 ) ;
#13415=LINE ( 'NONE', #95957, #64263 ) ;
#13431=CARTESIAN_POINT ( 'NONE',  ( -0.04725809328185200109, 9.175759667312519241, -8.057670357645360326 ) ) ;
#13525=AXIS2_PLACEMENT_3D ( 'NONE', #47873, #22595, #359 ) ;
#13625=ORIENTED_EDGE ( 'NONE', *, *, #38290, .F. ) ;
#13660=EDGE_LOOP ( 'NONE', ( #73843, #73595, #49294 ) ) ;
#13688=DIRECTION ( 'NONE',  ( 1.000000000000000000, 0.000000000000000000, 0.000000000000000000 ) ) ;
#13716=VECTOR ( 'NONE', #70342, 1000.000000000000000 ) ;
#13737=FACE_OUTER_BOUND ( 'NONE', #20437, .T. ) ;
#13765=CARTESIAN_POINT ( 'NONE',  ( 7.500000000000000888, -2.930060224340425901, -0.4701183149080217505 ) ) ;
#13833=ORIENTED_EDGE ( 'NONE', *, *, #56229, .T. ) ;
#13843=DIRECTION ( 'NONE',  ( -1.000000000000000000, 0.000000000000000000, 0.000000000000000000 ) ) ;
#13945=CARTESIAN_POINT ( 'NONE',  ( 0.2779000157839520702, 8.820699686765056668, -7.928862157988307402 ) ) ;
#13962=CARTESIAN_POINT ( 'NONE',  ( 7.847095227763524861, 4.129731495738483638, -7.493596212620240671 ) ) ;
#14017=ORIENTED_EDGE ( 'NONE', *, *, #4837, .T. ) ;
#14021=VECTOR ( 'NONE', #6836, 999.9999999999998863 ) ;
#14080=CARTESIAN_POINT ( 'NONE',  ( 7.500000000000000000, 0.7723602884924073431, -7.026388801734293033 ) ) ;
#14138=DIRECTION ( 'NONE',  ( -1.000000000000000000, 0.000000000000000000, 0.000000000000000000 ) ) ;
#14188=DIRECTION ( 'NONE',  ( 0.000000000000000000, 0.000000000000000000, 1.000000000000000000 ) ) ;
#14222=CARTESIAN_POINT ( 'NONE',  ( -4.250000000000000000, 5.204748896376250699E-16, -10.00000000000000000 ) ) ;
#14239=ADVANCED_FACE ( 'NONE', ( #75631 ), #35209, .F. ) ;
#14269=( BOUNDED_SURFACE ( )  B_SPLINE_SURFACE ( 3, 2, ( 
 ( #90296, #16406, #74098 ),
 ( #47701, #97852, #74629 ),
 ( #7242, #49288, #15879 ),
 ( #7773, #23473, #72517 ),
 ( #39649, #80600, #708 ),
 ( #24010, #33680, #57914 ),
 ( #186, #33151, #6723 ),
 ( #81646, #90837, #105424 ) ),
 .UNSPECIFIED., .F., .F., .F. ) 
 B_SPLINE_SURFACE_WITH_KNOTS ( ( 4, 2, 2, 4 ),
 ( 3, 3 ),
 ( 0.03851319102641419245, 0.04314724750133520914, 0.04546427573879571749, 0.04778130397625623277 ),
 ( 0.000000000000000000, 1.000000000000000000 ),
 .UNSPECIFIED. ) 
 GEOMETRIC_REPRESENTATION_ITEM ( )  RATIONAL_B_SPLINE_SURFACE ( (
 ( 1.000000000000000000, 0.8047781573724569482, 1.000000000000000000),
 ( 1.000000000000000000, 0.8123768202407029015, 1.000000000000000000),
 ( 1.000000000000000000, 0.8190667609308867059, 1.000000000000000000),
 ( 1.000000000000000000, 0.8191933927156084261, 1.000000000000000000),
 ( 1.000000000000000000, 0.8176088169850088683, 1.000000000000000000),
 ( 1.000000000000000000, 0.8122958474542694152, 1.000000000000000000),
 ( 1.000000000000000000, 0.8086309703845092622, 1.000000000000000000),
 ( 1.000000000000000000, 0.8047712409910817710, 1.000000000000000000) ) ) 
 REPRESENTATION_ITEM ( '' )  SURFACE ( )  );
#14326=DIRECTION ( 'NONE',  ( -0.000000000000000000, -0.000000000000000000, -1.000000000000000000 ) ) ;
#14360=VERTEX_POINT ( 'NONE', #29780 ) ;
#14437=CARTESIAN_POINT ( 'NONE',  ( 0.000000000000000000, 0.000000000000000000, -5.710657142857142432 ) ) ;
#14458=ORIENTED_EDGE ( 'NONE', *, *, #73235, .F. ) ;
#14466=CARTESIAN_POINT ( 'NONE',  ( 3.750000000000004885, -6.495190528383287365, 1.734723475976807094E-15 ) ) ;
#14468=ADVANCED_FACE ( 'NONE', ( #656 ), #64675, .F. ) ;
#14484=CARTESIAN_POINT ( 'NONE',  ( 6.658902113223476249, 5.287118297638405018, -7.776713651266118354 ) ) ;
#14675=ORIENTED_EDGE ( 'NONE', *, *, #21063, .F. ) ;
#14749=DIRECTION ( 'NONE',  ( -1.000000000000000000, 0.000000000000000000, 0.000000000000000000 ) ) ;
#14798=CARTESIAN_POINT ( 'NONE',  ( 7.500000000000000000, 2.575910028905302074, -0.3641256808890085961 ) ) ;
#14851=CIRCLE ( 'NONE', #23429, 4.250000000000000000 ) ;
#14864=CONICAL_SURFACE ( 'NONE', #42436, 7.500000000000000888, 0.8594454914424817238 ) ;
#14923=LINE ( 'NONE', #48353, #14021 ) ;
#14965=CARTESIAN_POINT ( 'NONE',  ( 4.250000000000000000, 0.000000000000000000, -9.078441367943003826 ) ) ;
#14983=CARTESIAN_POINT ( 'NONE',  ( 0.000000000000000000, 0.000000000000000000, 0.000000000000000000 ) ) ;
#15040=DIRECTION ( 'NONE',  ( 0.000000000000000000, 0.000000000000000000, -1.000000000000000000 ) ) ;
#15278=LINE ( 'NONE', #71924, #43071 ) ;
#15342=CARTESIAN_POINT ( 'NONE',  ( 7.970070017554211184, -4.546953124339766283, -8.057670357645358550 ) ) ;
#15368=DIRECTION ( 'NONE',  ( -0.000000000000000000, 0.000000000000000000, -1.000000000000000000 ) ) ;
#15437=ORIENTED_EDGE ( 'NONE', *, *, #51035, .T. ) ;
#15450=CARTESIAN_POINT ( 'NONE',  ( -0.6508621380849229920, -8.763657152406457485, -7.907633014911229274 ) ) ;
#15528=DIRECTION ( 'NONE',  ( -0.8191520442889975717, 0.000000000000000000, -0.5735764363510378328 ) ) ;
#15537=DIRECTION ( 'NONE',  ( 0.000000000000000000, 0.000000000000000000, 1.000000000000000000 ) ) ;
#15543=CARTESIAN_POINT ( 'NONE',  ( 0.3470952277635269700, 8.860649561028099086, -7.493596212620244224 ) ) ;
#15571=CARTESIAN_POINT ( 'NONE',  ( -7.500000000000000000, 4.330127018922188320, -10.00000000000000000 ) ) ;
#15616=AXIS2_PLACEMENT_3D ( 'NONE', #50620, #81933, #106747 ) ;
#15738=CARTESIAN_POINT ( 'NONE',  ( -7.894787914004607998, 0.7647108141804102033, -7.591390474663421983 ) ) ;
#15879=CARTESIAN_POINT ( 'NONE',  ( -7.894955577759743548, 1.603085139993701169, -7.593799241562211755 ) ) ;
#15905=ORIENTED_EDGE ( 'NONE', *, *, #19217, .T. ) ;
#15918=AXIS2_PLACEMENT_3D ( 'NONE', #35235, #101542, #99934 ) ;
#16078=CARTESIAN_POINT ( 'NONE',  ( -2.459698528280935381, 7.240146430416063872, -0.09933465333850977075 ) ) ;
#16093=CARTESIAN_POINT ( 'NONE',  ( 7.808623696107068746, -4.508310992948072915, -7.999704684617485739 ) ) ;
#16117=MECHANICAL_DESIGN_GEOMETRIC_PRESENTATION_REPRESENTATION('',(#95366),#10954);
#16319=DIRECTION ( 'NONE',  ( 0.000000000000000000, 0.000000000000000000, 1.000000000000000000 ) ) ;
#16333=B_SPLINE_CURVE_WITH_KNOTS ( 'NONE', 3,
 ( #77147, #43187, #18401, #93867, #60461, #36204 ),
 .UNSPECIFIED., .F., .F.,
 ( 4, 2, 4 ),
 ( 0.000000000000000000, 0.0004189869898914156798, 0.0008379739797828313595 ),
 .UNSPECIFIED. ) ;
#16402=CARTESIAN_POINT ( 'NONE',  ( 2.352174619733123695, -7.302225387960472602, -7.450218641349906967 ) ) ;
#16406=CARTESIAN_POINT ( 'NONE',  ( -7.499999999999999112, 4.651022038490012278, -7.928862870699868282 ) ) ;
#16482=AXIS2_PLACEMENT_3D ( 'NONE', #9824, #83195, #50811 ) ;
#16548=AXIS2_PLACEMENT_3D ( 'NONE', #67621, #12016, #36874 ) ;
#16587=LINE ( 'NONE', #39817, #102213 ) ;
#16736=EDGE_CURVE ( 'NONE', #77573, #106581, #93271, .T. ) ;
#16785=ORIENTED_EDGE ( 'NONE', *, *, #96237, .F. ) ;
#16801=ORIENTED_EDGE ( 'NONE', *, *, #24809, .F. ) ;
#16950=CARTESIAN_POINT ( 'NONE',  ( 4.406466114818337942, -6.116179640279066909, -7.446478553994767324 ) ) ;
#16996=DIRECTION ( 'NONE',  ( -0.000000000000000000, 0.000000000000000000, -1.000000000000000000 ) ) ;
#17001=EDGE_LOOP ( 'NONE', ( #20340, #17878, #92691, #73566 ) ) ;
#17099=EDGE_LOOP ( 'NONE', ( #18099, #85694 ) ) ;
#17122=ORIENTED_EDGE ( 'NONE', *, *, #26387, .F. ) ;
#17146=ADVANCED_FACE ( 'NONE', ( #51067 ), #93823, .F. ) ;
#17167=CARTESIAN_POINT ( 'NONE',  ( -10.12668159690567649, 1.256356190803089060E-15, -10.00000000000000000 ) ) ;
#17185=CIRCLE ( 'NONE', #10310, 4.250000000000000000 ) ;
#17202=DIRECTION ( 'NONE',  ( 0.000000000000000000, 0.000000000000000000, 1.000000000000000000 ) ) ;
#17211=CIRCLE ( 'NONE', #77497, 5.000000000000000000 ) ;
#17319=CARTESIAN_POINT ( 'NONE',  ( 0.6511518506208968660, -8.763486134561278007, -7.907570769506055086 ) ) ;
#17446=CONICAL_SURFACE ( 'NONE', #43297, 4.250000000000000000, 0.9599310885968754814 ) ;
#17458=ORIENTED_EDGE ( 'NONE', *, *, #8972, .T. ) ;
#17517=EDGE_CURVE ( 'NONE', #32589, #96921, #78172, .T. ) ;
#17528=MANIFOLD_SOLID_BREP ( 'ThdSchPat', #4966 ) ;
#17533=EDGE_CURVE ( 'NONE', #96921, #32589, #50584, .T. ) ;
#17543=EDGE_CURVE ( 'NONE', #60305, #27490, #17920, .T. ) ;
#17603=CARTESIAN_POINT ( 'NONE',  ( -5.047120108843201614, 5.746297884371388776, -0.1007566405101762153 ) ) ;
#17638=ORIENTED_EDGE ( 'NONE', *, *, #17533, .F. ) ;
#17642=CARTESIAN_POINT ( 'NONE',  ( 6.874999999999998224, 4.690970937165705124, -7.298562697733106397 ) ) ;
#17661=LINE ( 'NONE', #40855, #59595 ) ;
#17691=CARTESIAN_POINT ( 'NONE',  ( -7.922281120364393914, -4.573931137438282057, -8.047472243342934206 ) ) ;
#17723=EDGE_LOOP ( 'NONE', ( #13149, #24165, #59547, #43121 ) ) ;
#17731=DIRECTION ( 'NONE',  ( -1.000000000000000000, 0.000000000000000000, 0.000000000000000000 ) ) ;
#17744=EDGE_CURVE ( 'NONE', #45380, #54954, #76289, .T. ) ;
#17754=CARTESIAN_POINT ( 'NONE',  ( 0.000000000000000000, 0.000000000000000000, -9.078441367943003826 ) ) ;
#17827=CARTESIAN_POINT ( 'NONE',  ( -7.922281120364393914, 4.573931137438267847, -8.047472243342932430 ) ) ;
#17858=VERTEX_POINT ( 'NONE', #90093 ) ;
#17878=ORIENTED_EDGE ( 'NONE', *, *, #77608, .T. ) ;
#17920=CIRCLE ( 'NONE', #71246, 4.250000000000000000 ) ;
#17987=DIRECTION ( 'NONE',  ( 1.000000000000000000, 0.000000000000000000, 0.000000000000000000 ) ) ;
#18037=CARTESIAN_POINT ( 'NONE',  ( 7.500000000000000000, -4.330127018922200755, -7.422398894150036064 ) ) ;
#18045=VECTOR ( 'NONE', #105301, 999.9999999999998863 ) ;
#18057=FACE_OUTER_BOUND ( 'NONE', #8272, .T. ) ;
#18099=ORIENTED_EDGE ( 'NONE', *, *, #55769, .F. ) ;
#18216=DIRECTION ( 'NONE',  ( 1.000000000000000000, 0.000000000000000000, 0.000000000000000000 ) ) ;
#18217=CARTESIAN_POINT ( 'NONE',  ( -2.411464220262661495, -7.267994521134594876, -7.491772860716523930 ) ) ;
#18234=EDGE_CURVE ( 'NONE', #77573, #4416, #31752, .T. ) ;
#18280=CARTESIAN_POINT ( 'NONE',  ( 0.000000000000000000, 0.000000000000000000, -10.00000000000000000 ) ) ;
#18309=EDGE_LOOP ( 'NONE', ( #93845, #100648, #29032, #6651 ) ) ;
#18346=VERTEX_POINT ( 'NONE', #44083 ) ;
#18348=DIRECTION ( 'NONE',  ( 0.000000000000000000, 0.000000000000000000, -1.000000000000000000 ) ) ;
#18381=VERTEX_POINT ( 'NONE', #100180 ) ;
#18401=CARTESIAN_POINT ( 'NONE',  ( 6.070808553811512019E-16, -8.716842316802404511, -7.700127545397318585 ) ) ;
#18450=CARTESIAN_POINT ( 'NONE',  ( 0.000000000000000000, 0.000000000000000000, -4.814498510800145681 ) ) ;
#18455=CARTESIAN_POINT ( 'NONE',  ( 7.500000000000000888, 3.608439182435154269, -7.298562697733107285 ) ) ;
#18470=CARTESIAN_POINT ( 'NONE',  ( -7.500000000000000000, -4.330127018922203419, -0.9999999999999974465 ) ) ;
#18486=ORIENTED_EDGE ( 'NONE', *, *, #3730, .T. ) ;
#18611=ORIENTED_EDGE ( 'NONE', *, *, #56229, .F. ) ;
#18637=CARTESIAN_POINT ( 'NONE',  ( 6.250000000000000000, -5.051814855409235250, -7.198902722707430257 ) ) ;
#18676=CARTESIAN_POINT ( 'NONE',  ( -10.12668159690567826, 1.240160820363494750E-15, -9.226681596905679683 ) ) ;
#18685=CARTESIAN_POINT ( 'NONE',  ( -3.750000000000007105, 6.495190528383286477, 1.734723475976807094E-15 ) ) ;
#18761=CARTESIAN_POINT ( 'NONE',  ( 0.000000000000000000, 0.000000000000000000, -1.971869939371574620 ) ) ;
#18784=DIRECTION ( 'NONE',  ( -1.000000000000000000, 0.000000000000000000, 0.000000000000000000 ) ) ;
#18785=CARTESIAN_POINT ( 'NONE',  ( -7.894787914004607998, -0.7661396099416337702, -7.591390474663430865 ) ) ;
#18809=EDGE_CURVE ( 'NONE', #87281, #12410, #30209, .T. ) ;
#18825=CYLINDRICAL_SURFACE ( 'NONE', #35461, 4.250000000000000000 ) ;
#18857=CONICAL_SURFACE ( 'NONE', #61959, 7.500000000000000888, 0.8594454914424817238 ) ;
#18975=CARTESIAN_POINT ( 'NONE',  ( -5.000000000000000888, 6.123233995736767268E-16, -10.00000000000000000 ) ) ;
#19017=CIRCLE ( 'NONE', #99948, 5.000000000000000000 ) ;
#19053=CARTESIAN_POINT ( 'NONE',  ( 4.250000000000000000, 0.000000000000000000, -6.606815774914157835 ) ) ;
#19145=EDGE_LOOP ( 'NONE', ( #32458, #18611, #79259, #85408 ) ) ;
#19150=CARTESIAN_POINT ( 'NONE',  ( 7.894787914004607998, 0.7661396099416308836, -7.591390474663430865 ) ) ;
#19217=EDGE_CURVE ( 'NONE', #104354, #69179, #26033, .T. ) ;
#19252=DIRECTION ( 'NONE',  ( -0.5000000000000008882, 0.8660254037844381525, 0.000000000000000000 ) ) ;
#19291=CARTESIAN_POINT ( 'NONE',  ( 0.000000000000000000, 0.000000000000000000, -8.553285714285713937 ) ) ;
#19393=CARTESIAN_POINT ( 'NONE',  ( 2.599973688629601546E-12, 9.016154170237600241, -7.999534413642741093 ) ) ;
#19429=ORIENTED_EDGE ( 'NONE', *, *, #24809, .T. ) ;
#19442=ORIENTED_EDGE ( 'NONE', *, *, #81070, .T. ) ;
#19483=EDGE_LOOP ( 'NONE', ( #19995, #41372, #49539, #25761 ) ) ;
#19530=LINE ( 'NONE', #101984, #5894 ) ;
#19561=EDGE_CURVE ( 'NONE', #60305, #84586, #14923, .T. ) ;
#19662=ORIENTED_EDGE ( 'NONE', *, *, #77900, .F. ) ;
#19763=CARTESIAN_POINT ( 'NONE',  ( -5.000000000000000000, 0.000000000000000000, -7.131971428571428184 ) ) ;
#19809=CARTESIAN_POINT ( 'NONE',  ( 4.250000000000000000, 0.000000000000000000, -10.00000000000000000 ) ) ;
#19828=ORIENTED_EDGE ( 'NONE', *, *, #68519, .T. ) ;
#19888=DIRECTION ( 'NONE',  ( -1.000000000000000000, 0.000000000000000000, 0.000000000000000000 ) ) ;
#19904=VECTOR ( 'NONE', #1423, 1000.000000000000000 ) ;
#19995=ORIENTED_EDGE ( 'NONE', *, *, #59964, .F. ) ;
#20071=CONICAL_SURFACE ( 'NONE', #51024, 4.174999999999998934, 0.9599310885968824758 ) ;
#20100=AXIS2_PLACEMENT_3D ( 'NONE', #93616, #43993, #35404 ) ;
#20126=AXIS2_PLACEMENT_3D ( 'NONE', #46726, #32151, #80670 ) ;
#20186=EDGE_LOOP ( 'NONE', ( #71839, #7962, #42258, #10191 ) ) ;
#20209=EDGE_LOOP ( 'NONE', ( #56510, #97625, #40502, #87143 ) ) ;
#20254=PRODUCT_CONTEXT ( 'NONE', #106482, 'mechanical' ) ;
#20259=AXIS2_PLACEMENT_3D ( 'NONE', #5306, #80765, #70031 ) ;
#20281=DIRECTION ( 'NONE',  ( -1.000000000000000000, 0.000000000000000000, 0.000000000000000000 ) ) ;
#20340=ORIENTED_EDGE ( 'NONE', *, *, #68519, .F. ) ;
#20346=CIRCLE ( 'NONE', #25473, 4.250000000000000000 ) ;
#20352=EDGE_LOOP ( 'NONE', ( #102665, #21127, #16785, #103335 ) ) ;
#20392=CARTESIAN_POINT ( 'NONE',  ( -7.500000000000000000, 4.330127018922188320, -7.422398894150033399 ) ) ;
#20437=EDGE_LOOP ( 'NONE', ( #59810, #89478, #19442, #74789 ) ) ;
#20568=EDGE_CURVE ( 'NONE', #31711, #73538, #99512, .T. ) ;
#20626=VECTOR ( 'NONE', #12140, 1000.000000000000000 ) ;
#20635=CARTESIAN_POINT ( 'NONE',  ( -5.040301471719076609, -5.750234626350522404, -0.09933465333851672352 ) ) ;
#20690=EDGE_CURVE ( 'NONE', #34113, #18346, #53110, .T. ) ;
#20704=ORIENTED_EDGE ( 'NONE', *, *, #94830, .F. ) ;
#20720=LINE ( 'NONE', #4475, #80861 ) ;
#20881=VECTOR ( 'NONE', #88004, 1000.000000000000000 ) ;
#20886=DIRECTION ( 'NONE',  ( -1.000000000000000000, 0.000000000000000000, 0.000000000000000000 ) ) ;
#20907=VERTEX_POINT ( 'NONE', #21774 ) ;
#20962=VERTEX_POINT ( 'NONE', #33050 ) ;
#21063=EDGE_CURVE ( 'NONE', #12410, #18381, #37669, .T. ) ;
#21127=ORIENTED_EDGE ( 'NONE', *, *, #75483, .T. ) ;
#21157=DIRECTION ( 'NONE',  ( 0.000000000000000000, 0.000000000000000000, -1.000000000000000000 ) ) ;
#21296=AXIS2_PLACEMENT_3D ( 'NONE', #94791, #4170, #37102 ) ;
#21380=AXIS2_PLACEMENT_3D ( 'NONE', #35680, #43202, #101960 ) ;
#21448=ORIENTED_EDGE ( 'NONE', *, *, #43266, .F. ) ;
#21516=DIRECTION ( 'NONE',  ( 0.8660254037844382635, 0.5000000000000006661, 0.000000000000000000 ) ) ;
#21519=CONICAL_SURFACE ( 'NONE', #95550, 4.250000000000000000, 0.9599310885968754814 ) ;
#21571=CARTESIAN_POINT ( 'NONE',  ( 0.3875187462253061321, 8.436519985394745902, -7.781689322727966207 ) ) ;
#21602=DIRECTION ( 'NONE',  ( -0.000000000000000000, -0.000000000000000000, -1.000000000000000000 ) ) ;
#21659=CARTESIAN_POINT ( 'NONE',  ( 0.000000000000000000, 0.000000000000000000, -7.131971428571428184 ) ) ;
#21661=CARTESIAN_POINT ( 'NONE',  ( 3.750000000000007105, 6.495190528383288253, 1.734723475976807094E-15 ) ) ;
#21671=ORIENTED_EDGE ( 'NONE', *, *, #101985, .F. ) ;
#21770=DIRECTION ( 'NONE',  ( 1.000000000000000000, 0.000000000000000000, 0.000000000000000000 ) ) ;
#21774=CARTESIAN_POINT ( 'NONE',  ( 7.894787914004607998, 1.238680740843649375E-13, -7.591390474663426424 ) ) ;
#21877=CARTESIAN_POINT ( 'NONE',  ( 7.499999999999999112, 1.854554393013827518, -0.1880126015361714420 ) ) ;
#22096=CARTESIAN_POINT ( 'NONE',  ( 6.523606932381285084, 4.893847819346740735, -7.213065638940823199 ) ) ;
#22112=EDGE_LOOP ( 'NONE', ( #87473, #34980, #95910, #14017, #23754 ) ) ;
#22139=CIRCLE ( 'NONE', #90960, 5.000000000000000000 ) ;
#22168=FACE_OUTER_BOUND ( 'NONE', #28813, .T. ) ;
#22225=CARTESIAN_POINT ( 'NONE',  ( 7.894958282449376696, -1.603399432393033397, -7.593838100136811597 ) ) ;
#22228=CARTESIAN_POINT ( 'NONE',  ( -10.39117206796836257, 0.000000000000000000, -8.500000000000000000 ) ) ;
#22371=LINE ( 'NONE', #14222, #32397 ) ;
#22380=AXIS2_PLACEMENT_3D ( 'NONE', #103178, #62723, #14138 ) ;
#22401=VERTEX_POINT ( 'NONE', #71464 ) ;
#22496=CARTESIAN_POINT ( 'NONE',  ( 0.000000000000000000, 0.000000000000000000, -4.814498510800145681 ) ) ;
#22595=DIRECTION ( 'NONE',  ( -0.000000000000000000, -0.000000000000000000, -1.000000000000000000 ) ) ;
#22660=AXIS2_PLACEMENT_3D ( 'NONE', #47727, #15368, #97879 ) ;
#22676=ORIENTED_EDGE ( 'NONE', *, *, #32633, .T. ) ;
#22706=DIRECTION ( 'NONE',  ( 0.000000000000000000, 0.000000000000000000, -1.000000000000000000 ) ) ;
#22897=DIRECTION ( 'NONE',  ( 0.000000000000000000, 0.000000000000000000, -1.000000000000000000 ) ) ;
#22932=CARTESIAN_POINT ( 'NONE',  ( 7.500000000000000888, 0.7513028741560163759, -0.02472015219302733588 ) ) ;
#22941=ADVANCED_FACE ( 'NONE', ( #101601 ), #87023, .F. ) ;
#22952=ORIENTED_EDGE ( 'NONE', *, *, #7530, .F. ) ;
#23008=VERTEX_POINT ( 'NONE', #6602 ) ;
#23048=DIRECTION ( 'NONE',  ( 0.000000000000000000, 0.000000000000000000, 1.000000000000000000 ) ) ;
#23067=DIRECTION ( 'NONE',  ( 1.000000000000000000, 0.000000000000000000, 0.000000000000000000 ) ) ;
#23071=CARTESIAN_POINT ( 'NONE',  ( 0.000000000000000000, 0.000000000000000000, -9.078441367943003826 ) ) ;
#23107=DIRECTION ( 'NONE',  ( -1.000000000000000000, 0.000000000000000000, 0.000000000000000000 ) ) ;
#23188=EDGE_CURVE ( 'NONE', #94271, #64087, #92298, .T. ) ;
#23209=DIRECTION ( 'NONE',  ( 0.9396926207859143121, 1.150791560227857665E-16, -0.3420201433256525592 ) ) ;
#23429=AXIS2_PLACEMENT_3D ( 'NONE', #10938, #2860, #35814 ) ;
#23436=ADVANCED_FACE ( 'NONE', ( #54476 ), #33740, .F. ) ;
#23468=CARTESIAN_POINT ( 'NONE',  ( -0.3470952277635213634, -8.860649561028106191, -7.493596212620246888 ) ) ;
#23473=CARTESIAN_POINT ( 'NONE',  ( -7.500000000000000000, -0.7583608255792044783, -7.446489218764574147 ) ) ;
#23496=ORIENTED_EDGE ( 'NONE', *, *, #23188, .T. ) ;
#23546=ADVANCED_FACE ( 'NONE', ( #67782 ), #25276, .F. ) ;
#23709=ORIENTED_EDGE ( 'NONE', *, *, #25142, .T. ) ;
#23754=ORIENTED_EDGE ( 'NONE', *, *, #5978, .T. ) ;
#23795=ORIENTED_EDGE ( 'NONE', *, *, #101977, .T. ) ;
#23803=ADVANCED_FACE ( 'NONE', ( #48786 ), #20071, .F. ) ;
#23824=CARTESIAN_POINT ( 'NONE',  ( 7.500000000000000000, 3.948247735265644653, -7.349893093596817195 ) ) ;
#23921=ORIENTED_EDGE ( 'NONE', *, *, #78440, .F. ) ;
#24010=CARTESIAN_POINT ( 'NONE',  ( -7.500000000000000000, -3.160302461882437797, -7.231849989190477501 ) ) ;
#24026=DIRECTION ( 'NONE',  ( 1.000000000000000000, 0.000000000000000000, 0.000000000000000000 ) ) ;
#24027=CARTESIAN_POINT ( 'NONE',  ( -7.500000000000000888, 2.575910028905293192, -0.3641256808890049879 ) ) ;
#24037=ORIENTED_EDGE ( 'NONE', *, *, #74896, .T. ) ;
#24155=ORIENTED_EDGE ( 'NONE', *, *, #4678, .F. ) ;
#24165=ORIENTED_EDGE ( 'NONE', *, *, #84381, .F. ) ;
#24184=DIRECTION ( 'NONE',  ( -0.000000000000000000, -0.000000000000000000, -1.000000000000000000 ) ) ;
#24186=EDGE_LOOP ( 'NONE', ( #90789, #26175, #84489, #70840 ) ) ;
#24194=CARTESIAN_POINT ( 'NONE',  ( -5.000000000000000000, 0.000000000000000000, -1.446714285714285841 ) ) ;
#24233=AXIS2_PLACEMENT_3D ( 'NONE', #70826, #70299, #103196 ) ;
#24589=DIRECTION ( 'NONE',  ( 0.000000000000000000, 0.000000000000000000, 1.000000000000000000 ) ) ;
#24642=CARTESIAN_POINT ( 'NONE',  ( -4.606548227981508425, -6.456511556909262595, -7.591235721156640359 ) ) ;
#24704=( BOUNDED_SURFACE ( )  B_SPLINE_SURFACE ( 3, 2, ( 
 ( #36828, #103122, #62153 ),
 ( #102589, #96089, #104165 ),
 ( #5997, #30307, #22225 ),
 ( #14080, #28738, #38920 ),
 ( #61623, #72335, #48040 ),
 ( #41559, #8652, #24865 ),
 ( #23824, #31382, #97132 ),
 ( #82551, #8118, #57721 ) ),
 .UNSPECIFIED., .F., .F., .F. ) 
 B_SPLINE_SURFACE_WITH_KNOTS ( ( 4, 2, 2, 4 ),
 ( 3, 3 ),
 ( 0.03850042371095790256, 0.04313406099830587037, 0.04545087964197985081, 0.04776769828565383125 ),
 ( 0.000000000000000000, 1.000000000000000000 ),
 .UNSPECIFIED. ) 
 GEOMETRIC_REPRESENTATION_ITEM ( )  RATIONAL_B_SPLINE_SURFACE ( (
 ( 1.000000000000000000, 0.8047781847388131293, 1.000000000000000000),
 ( 1.000000000000000000, 0.8123760230790857406, 1.000000000000000000),
 ( 1.000000000000000000, 0.8190653851699112309, 1.000000000000000000),
 ( 1.000000000000000000, 0.8191940386277110075, 1.000000000000000000),
 ( 1.000000000000000000, 0.8176096570055705337, 1.000000000000000000),
 ( 1.000000000000000000, 0.8122964723277524834, 1.000000000000000000),
 ( 1.000000000000000000, 0.8086312464132838773, 1.000000000000000000),
 ( 1.000000000000000000, 0.8047712192439641088, 1.000000000000000000) ) ) 
 REPRESENTATION_ITEM ( '' )  SURFACE ( )  );
#24714=CARTESIAN_POINT ( 'NONE',  ( -3.093533885184728494, -6.874201416485484550, -7.446478553994769101 ) ) ;
#24771=DIRECTION ( 'NONE',  ( 0.000000000000000000, 0.000000000000000000, 1.000000000000000000 ) ) ;
#24809=EDGE_CURVE ( 'NONE', #23008, #81667, #86929, .T. ) ;
#24834=CARTESIAN_POINT ( 'NONE',  ( -2.500000000000000444, -7.216878364870336959, -7.063244554130006847 ) ) ;
#24865=CARTESIAN_POINT ( 'NONE',  ( 7.908217798048221781, 3.084840533507049454, -7.795645399445158219 ) ) ;
#24961=VERTEX_POINT ( 'NONE', #59327 ) ;
#25006=EDGE_CURVE ( 'NONE', #2343, #13350, #9155, .T. ) ;
#25015=FACE_OUTER_BOUND ( 'NONE', #19145, .T. ) ;
#25046=AXIS2_PLACEMENT_3D ( 'NONE', #23, #58299, #82577 ) ;
#25061=ADVANCED_FACE ( 'NONE', ( #25015 ), #25565, .F. ) ;
#25112=ORIENTED_EDGE ( 'NONE', *, *, #42507, .F. ) ;
#25120=DIRECTION ( 'NONE',  ( 0.000000000000000000, 0.000000000000000000, 1.000000000000000000 ) ) ;
#25142=EDGE_CURVE ( 'NONE', #96921, #81667, #100464, .T. ) ;
#25221=ORIENTED_EDGE ( 'NONE', *, *, #105350, .F. ) ;
#25276=CONICAL_SURFACE ( 'NONE', #85552, 4.250000000000000000, 0.9599310885968754814 ) ;
#25437=DIRECTION ( 'NONE',  ( -0.000000000000000000, -0.000000000000000000, -1.000000000000000000 ) ) ;
#25447=DIRECTION ( 'NONE',  ( 0.8191520442889884679, 0.000000000000000000, 0.5735764363510508224 ) ) ;
#25473=AXIS2_PLACEMENT_3D ( 'NONE', #4256, #85722, #84643 ) ;
#25513=AXIS2_PLACEMENT_3D ( 'NONE', #103549, #21602, #10797 ) ;
#25565=CYLINDRICAL_SURFACE ( 'NONE', #88911, 5.000000000000000888 ) ;
#25603=CARTESIAN_POINT ( 'NONE',  ( 7.500000000000000000, 4.330127018922189208, -10.00000000000000000 ) ) ;
#25605=CARTESIAN_POINT ( 'NONE',  ( 7.112481253775658985, -4.553861071372089064, -7.781689322727664226 ) ) ;
#25641=CARTESIAN_POINT ( 'NONE',  ( 7.897836333153806621, 1.530409084195003100, -7.633857274177628049 ) ) ;
#25699=CARTESIAN_POINT ( 'NONE',  ( -7.500000000000000000, -3.988190556646209917, -0.8526458641284285767 ) ) ;
#25723=CARTESIAN_POINT ( 'NONE',  ( 4.250000000000000000, 0.000000000000000000, -9.078441367943003826 ) ) ;
#25761=ORIENTED_EDGE ( 'NONE', *, *, #89741, .F. ) ;
#25824=CARTESIAN_POINT ( 'NONE',  ( -4.406466114815700941, 6.116179640280957841, -7.446478553995463656 ) ) ;
#25865=AXIS2_PLACEMENT_3D ( 'NONE', #72533, #54209, #5162 ) ;
#25942=DIRECTION ( 'NONE',  ( 0.000000000000000000, 0.000000000000000000, 1.000000000000000000 ) ) ;
#26033=CIRCLE ( 'NONE', #1858, 4.981862520314373377 ) ;
#26064=AXIS2_PLACEMENT_3D ( 'NONE', #6336, #39278, #72156 ) ;
#26081=CARTESIAN_POINT ( 'NONE',  ( -1.250000000000000888, 7.938566201357359020, -7.198902722707429369 ) ) ;
#26082=ADVANCED_FACE ( 'NONE', ( #81883 ), #56549, .T. ) ;
#26087=CARTESIAN_POINT ( 'NONE',  ( -7.922281120364393914, -4.573931137438282057, -8.047472243342934206 ) ) ;
#26106=CARTESIAN_POINT ( 'NONE',  ( 0.000000000000000000, 0.000000000000000000, -25.03750572909317285 ) ) ;
#26112=B_SPLINE_CURVE_WITH_KNOTS ( 'NONE', 3,
 ( #83008, #19393, #42540, #52225, #36103, #68973 ),
 .UNSPECIFIED., .F., .F.,
 ( 4, 2, 4 ),
 ( -5.145455527293658110E-06, 0.0004153350442917327912, 0.0008358155441107592218 ),
 .UNSPECIFIED. ) ;
#26175=ORIENTED_EDGE ( 'NONE', *, *, #85732, .T. ) ;
#26202=DIRECTION ( 'NONE',  ( -1.000000000000000000, 0.000000000000000000, 0.000000000000000000 ) ) ;
#26323=CONICAL_SURFACE ( 'NONE', #86579, 5.000000000000000000, 0.9599310885968913576 ) ;
#26387=EDGE_CURVE ( 'NONE', #57728, #9383, #6427, .T. ) ;
#26476=CARTESIAN_POINT ( 'NONE',  ( -7.264118654998711122, 4.945491722146218017, -7.907633014911222169 ) ) ;
#26501=CARTESIAN_POINT ( 'NONE',  ( 7.264118654998712010, -4.945491722146226898, -7.907633014911222169 ) ) ;
#26571=AXIS2_PLACEMENT_3D ( 'NONE', #63023, #39287, #63564 ) ;
#26591=EDGE_CURVE ( 'NONE', #52946, #82359, #71893, .T. ) ;
#26595=CYLINDRICAL_SURFACE ( 'NONE', #57596, 4.250000000000000000 ) ;
#26621=ORIENTED_EDGE ( 'NONE', *, *, #75483, .F. ) ;
#26624=DIRECTION ( 'NONE',  ( -0.8191520442889975717, 0.000000000000000000, -0.5735764363510378328 ) ) ;
#26730=CARTESIAN_POINT ( 'NONE',  ( 4.250000000000000000, 0.000000000000000000, -3.764187203485586330 ) ) ;
#26769=VERTEX_POINT ( 'NONE', #53921 ) ;
#26793=PLANE ( 'NONE',  #48037 ) ;
#26814=VERTEX_POINT ( 'NONE', #73279 ) ;
#26878=CARTESIAN_POINT ( 'NONE',  ( -7.914973979435151463, -3.817460047930454348, -7.907502498112421563 ) ) ;
#27044=CARTESIAN_POINT ( 'NONE',  ( -4.250000000000000000, 5.204748896376250699E-16, -9.449444346342716017 ) ) ;
#27130=CIRCLE ( 'NONE', #9823, 4.250000000000000000 ) ;
#27152=ADVANCED_FACE ( 'NONE', ( #92133 ), #2055, .F. ) ;
#27190=CARTESIAN_POINT ( 'NONE',  ( 5.000000000000000000, 6.123233995736766282E-16, -8.553285714285713937 ) ) ;
#27407=CONICAL_SURFACE ( 'NONE', #1460, 10.39117206796836257, 1.221730476396047926 ) ;
#27448=ORIENTED_EDGE ( 'NONE', *, *, #25142, .F. ) ;
#27490=VERTEX_POINT ( 'NONE', #8308 ) ;
#27520=ADVANCED_FACE ( 'NONE', ( #32084 ), #14269, .F. ) ;
#27550=VERTEX_POINT ( 'NONE', #106467 ) ;
#27633=CARTESIAN_POINT ( 'NONE',  ( 0.000000000000000000, 0.000000000000000000, -10.00000000000000000 ) ) ;
#27658=FACE_BOUND ( 'NONE', #17099, .T. ) ;
#27673=EDGE_CURVE ( 'NONE', #17858, #37257, #80665, .T. ) ;
#27677=LINE ( 'NONE', #12489, #10439 ) ;
#27697=B_SPLINE_CURVE_WITH_KNOTS ( 'NONE', 3,
 ( #48958, #89974, #16078, #64132, #97001, #89451 ),
 .UNSPECIFIED., .F., .F.,
 ( 4, 2, 4 ),
 ( 0.004444412883774330643, 0.006655097293744430265, 0.008865781703714530754 ),
 .UNSPECIFIED. ) ;
#27733=ORIENTED_EDGE ( 'NONE', *, *, #100030, .F. ) ;
#27749=CIRCLE ( 'NONE', #79429, 4.250000000000000000 ) ;
#27753=CONICAL_SURFACE ( 'NONE', #87995, 5.000000000000000000, 0.9599310885968913576 ) ;
#27760=CARTESIAN_POINT ( 'NONE',  ( -7.500000000000000888, 2.886751345948123326, -7.198902722707428481 ) ) ;
#27788=ORIENTED_EDGE ( 'NONE', *, *, #44999, .F. ) ;
#27802=EDGE_CURVE ( 'NONE', #20962, #81388, #63259, .T. ) ;
#27814=ORIENTED_EDGE ( 'NONE', *, *, #27673, .F. ) ;
#27987=ORIENTED_EDGE ( 'NONE', *, *, #60565, .F. ) ;
#28147=ORIENTED_EDGE ( 'NONE', *, *, #91657, .T. ) ;
#28205=CARTESIAN_POINT ( 'NONE',  ( -7.500000000000000000, -4.330127018922201643, -7.422398894150036064 ) ) ;
#28253=CARTESIAN_POINT ( 'NONE',  ( -3.750000000000007105, 6.495190528383286477, 1.734723475976807094E-15 ) ) ;
#28280=EDGE_LOOP ( 'NONE', ( #83904, #81409, #3547, #32017 ) ) ;
#28494=CARTESIAN_POINT ( 'NONE',  ( 0.000000000000000000, 0.000000000000000000, -9.974599999999998801 ) ) ;
#28654=EDGE_CURVE ( 'NONE', #90336, #35664, #76855, .T. ) ;
#28675=AXIS2_PLACEMENT_3D ( 'NONE', #49917, #7858, #48316 ) ;
#28692=CYLINDRICAL_SURFACE ( 'NONE', #40479, 4.250000000000000000 ) ;
#28738=CARTESIAN_POINT ( 'NONE',  ( 7.499999999999650058, 0.7577384720645206073, -7.446470314338821339 ) ) ;
#28743=ORIENTED_EDGE ( 'NONE', *, *, #42507, .T. ) ;
#28759=AXIS2_PLACEMENT_3D ( 'NONE', #62488, #67526, #21516 ) ;
#28794=LINE ( 'NONE', #27190, #50974 ) ;
#28813=EDGE_LOOP ( 'NONE', ( #46656, #99329, #83423 ) ) ;
#28829=DIRECTION ( 'NONE',  ( 0.000000000000000000, 0.000000000000000000, 1.000000000000000000 ) ) ;
#29004=CARTESIAN_POINT ( 'NONE',  ( 0.000000000000000000, 0.000000000000000000, -3.393184225085859929 ) ) ;
#29032=ORIENTED_EDGE ( 'NONE', *, *, #94907, .T. ) ;
#29132=ORIENTED_EDGE ( 'NONE', *, *, #27802, .F. ) ;
#29158=LINE ( 'NONE', #88412, #54790 ) ;
#29202=VECTOR ( 'NONE', #87479, 1000.000000000000000 ) ;
#29328=AXIS2_PLACEMENT_3D ( 'NONE', #79484, #29899, #30429 ) ;
#29364=CARTESIAN_POINT ( 'NONE',  ( 7.500000000000000000, 4.330127018922189208, -10.00000000000000000 ) ) ;
#29417=AXIS2_PLACEMENT_3D ( 'NONE', #73275, #96524, #81366 ) ;
#29518=VECTOR ( 'NONE', #8478, 1000.000000000000000 ) ;
#29616=PLANE ( 'NONE',  #28759 ) ;
#29627=DIRECTION ( 'NONE',  ( 0.000000000000000000, 0.000000000000000000, 1.000000000000000000 ) ) ;
#29674=CARTESIAN_POINT ( 'NONE',  ( 1.282512619719359481, 8.391164935523910628, -7.795653906408836598 ) ) ;
#29730=VERTEX_POINT ( 'NONE', #92689 ) ;
#29747=B_SPLINE_CURVE_WITH_KNOTS ( 'NONE', 3,
 ( #80385, #98684, #31357, #105724, #39430, #72303 ),
 .UNSPECIFIED., .F., .F.,
 ( 4, 2, 4 ),
 ( 0.004615310220740741730, 0.006918661718823352832, 0.009222013216905963068 ),
 .UNSPECIFIED. ) ;
#29780=CARTESIAN_POINT ( 'NONE',  ( -3.750000000000004441, -6.495190528383288253, 1.734723475976807094E-15 ) ) ;
#29899=DIRECTION ( 'NONE',  ( -0.000000000000000000, -0.000000000000000000, 1.000000000000000000 ) ) ;
#29987=CARTESIAN_POINT ( 'NONE',  ( -7.500000000000000888, 3.639598441879738910, -0.7155132341745207292 ) ) ;
#30135=CARTESIAN_POINT ( 'NONE',  ( 7.922281120364393914, 4.573931137438267847, -8.047472243342932430 ) ) ;
#30208=ORIENTED_EDGE ( 'NONE', *, *, #8972, .F. ) ;
#30209=B_SPLINE_CURVE_WITH_KNOTS ( 'NONE', 3,
 ( #58546, #10507, #98967, #1327, #91447, #49900, #18637, #91962, #51497 ),
 .UNSPECIFIED., .F., .F.,
 ( 4, 2, 1, 2, 4 ),
 ( 6.245710625686469831E-20, 0.002165063509461098799, 0.004330127018922196730, 0.006495190528383295095, 0.008660254037844391725 ),
 .UNSPECIFIED. ) ;
#30269=B_SPLINE_CURVE_WITH_KNOTS ( 'NONE', 3,
 ( #21661, #61045, #52934, #69659, #85860, #87442 ),
 .UNSPECIFIED., .F., .F.,
 ( 4, 2, 4 ),
 ( 0.004444412883774348857, 0.006655097293744438938, 0.008865781703714529019 ),
 .UNSPECIFIED. ) ;
#30280=CONICAL_SURFACE ( 'NONE', #59531, 5.000000000000000000, 0.9599310885968913576 ) ;
#30307=CARTESIAN_POINT ( 'NONE',  ( 7.500000000000698996, -1.614186302714018861, -7.450236204327475242 ) ) ;
#30308=AXIS2_PLACEMENT_3D ( 'NONE', #82420, #58687, #100195 ) ;
#30429=DIRECTION ( 'NONE',  ( 1.000000000000000000, 0.000000000000000000, 0.000000000000000000 ) ) ;
#30487=VERTEX_POINT ( 'NONE', #88997 ) ;
#30555=FACE_OUTER_BOUND ( 'NONE', #2168, .T. ) ;
#30557=B_SPLINE_CURVE_WITH_KNOTS ( 'NONE', 3,
 ( #14466, #95955, #31244, #46855, #86812, #78682 ),
 .UNSPECIFIED., .F., .F.,
 ( 4, 2, 4 ),
 ( 0.004444412883774324571, 0.006655097293744431132, 0.008865781703714535958 ),
 .UNSPECIFIED. ) ;
#30575=DIRECTION ( 'NONE',  ( -1.000000000000000000, 0.000000000000000000, 0.000000000000000000 ) ) ;
#30666=CARTESIAN_POINT ( 'NONE',  ( 0.000000000000000000, 0.000000000000000000, -10.00000000000000000 ) ) ;
#30729=DIRECTION ( 'NONE',  ( 0.8191520442889884679, 0.000000000000000000, 0.5735764363510508224 ) ) ;
#30875=EDGE_CURVE ( 'NONE', #81388, #49340, #22139, .T. ) ;
#30937=CARTESIAN_POINT ( 'NONE',  ( -4.250000000000000000, 5.204748896376250699E-16, -6.235812796514431433 ) ) ;
#30975=CIRCLE ( 'NONE', #61764, 4.250000000000000000 ) ;
#31034=CARTESIAN_POINT ( 'NONE',  ( 7.499999999999999112, 3.639598441879750901, -0.7155132341745242819 ) ) ;
#31101=CARTESIAN_POINT ( 'NONE',  ( 0.000000000000000000, 0.000000000000000000, -2.342872917771300578 ) ) ;
#31123=ADVANCED_FACE ( 'NONE', ( #70447 ), #27407, .T. ) ;
#31163=CIRCLE ( 'NONE', #86281, 5.000000000000000000 ) ;
#31204=DIRECTION ( 'NONE',  ( 1.000000000000000000, 0.000000000000000000, 0.000000000000000000 ) ) ;
#31244=CARTESIAN_POINT ( 'NONE',  ( 2.459698528280936269, -7.240146430416073642, -0.09933465333851825008 ) ) ;
#31292=EDGE_CURVE ( 'NONE', #34186, #35664, #41063, .T. ) ;
#31346=ORIENTED_EDGE ( 'NONE', *, *, #92666, .F. ) ;
#31357=CARTESIAN_POINT ( 'NONE',  ( 7.897850199329718990, -1.533397866934080422, -7.634054012537970557 ) ) ;
#31382=CARTESIAN_POINT ( 'NONE',  ( 7.500000000000000000, 3.882635837267457202, -7.781684861376771067 ) ) ;
#31433=CARTESIAN_POINT ( 'NONE',  ( -7.922281120364393914, 4.573931137438267847, -8.047472243342932430 ) ) ;
#31465=DIRECTION ( 'NONE',  ( 0.000000000000000000, -0.000000000000000000, 1.000000000000000000 ) ) ;
#31482=ORIENTED_EDGE ( 'NONE', *, *, #96237, .T. ) ;
#31488=CARTESIAN_POINT ( 'NONE',  ( 4.250000000000000000, 0.000000000000000000, -10.00000000000000000 ) ) ;
#31513=CARTESIAN_POINT ( 'NONE',  ( 0.000000000000000000, 0.000000000000000000, -0.5505556536572887572 ) ) ;
#31529=VECTOR ( 'NONE', #82403, 1000.000000000000000 ) ;
#31602=ADVANCED_FACE ( 'NONE', ( #60215 ), #26793, .T. ) ;
#31629=( BOUNDED_SURFACE ( )  B_SPLINE_SURFACE ( 3, 2, ( 
 ( #13962, #63073, #12899 ),
 ( #22096, #71151, #14484 ),
 ( #104044, #6403, #70630 ),
 ( #87881, #47397, #39338 ),
 ( #103521, #80290, #79243 ),
 ( #46871, #95432, #29674 ),
 ( #62544, #21571, #71669 ),
 ( #87354, #105121, #13431 ) ),
 .UNSPECIFIED., .F., .F., .F. ) 
 B_SPLINE_SURFACE_WITH_KNOTS ( ( 4, 2, 2, 4 ),
 ( 3, 3 ),
 ( 0.03861844051980969916, 0.04325213341840641879, 0.04556897986770477860, 0.04788582631700313841 ),
 ( 0.000000000000000000, 1.000000000000000000 ),
 .UNSPECIFIED. ) 
 GEOMETRIC_REPRESENTATION_ITEM ( )  RATIONAL_B_SPLINE_SURFACE ( (
 ( 1.000000000000000000, 0.8047781759831917903, 1.000000000000000000),
 ( 1.000000000000000000, 0.8123762462806505269, 1.000000000000000000),
 ( 1.000000000000000000, 0.8190659850614816495, 1.000000000000000000),
 ( 1.000000000000000000, 0.8191937571014599184, 1.000000000000000000),
 ( 1.000000000000000000, 0.8176092952779866474, 1.000000000000000000),
 ( 1.000000000000000000, 0.8122962088597071029, 1.000000000000000000),
 ( 1.000000000000000000, 0.8086311330827505861, 1.000000000000000000),
 ( 1.000000000000000000, 0.8047712282214324331, 1.000000000000000000) ) ) 
 REPRESENTATION_ITEM ( '' )  SURFACE ( )  );
#31672=ORIENTED_EDGE ( 'NONE', *, *, #44999, .T. ) ;
#31706=CONICAL_SURFACE ( 'NONE', #26571, 4.250000000000000000, 0.9599310885968754814 ) ;
#31711=VERTEX_POINT ( 'NONE', #53163 ) ;
#31720=CYLINDRICAL_SURFACE ( 'NONE', #62146, 4.250000000000000000 ) ;
#31734=ORIENTED_EDGE ( 'NONE', *, *, #81070, .F. ) ;
#31752=LINE ( 'NONE', #97502, #86902 ) ;
#31800=DIRECTION ( 'NONE',  ( -0.000000000000000000, 0.000000000000000000, -1.000000000000000000 ) ) ;
#31873=ORIENTED_EDGE ( 'NONE', *, *, #6941, .F. ) ;
#31999=EDGE_LOOP ( 'NONE', ( #26621, #53323, #104033, #51983 ) ) ;
#32017=ORIENTED_EDGE ( 'NONE', *, *, #60565, .T. ) ;
#32084=FACE_OUTER_BOUND ( 'NONE', #57524, .T. ) ;
#32096=CYLINDRICAL_SURFACE ( 'NONE', #105171, 4.250000000000000000 ) ;
#32108=EDGE_LOOP ( 'NONE', ( #36407, #17638, #23709, #49946 ) ) ;
#32117=ADVANCED_FACE ( 'NONE', ( #43868 ), #35821, .T. ) ;
#32122=FACE_OUTER_BOUND ( 'NONE', #47891, .T. ) ;
#32139=FILL_AREA_STYLE ('',( #71506 ) ) ;
#32151=DIRECTION ( 'NONE',  ( 0.000000000000000000, 0.000000000000000000, 1.000000000000000000 ) ) ;
#32160=CARTESIAN_POINT ( 'NONE',  ( -7.500000000000000888, -3.640541674360523228, -0.7158139487964588765 ) ) ;
#32174=DIRECTION ( 'NONE',  ( 1.000000000000000000, 0.000000000000000000, 0.000000000000000000 ) ) ;
#32240=ADVANCED_FACE ( 'NONE', ( #53559 ), #39537, .F. ) ;
#32369=VERTEX_POINT ( 'NONE', #8713 ) ;
#32397=VECTOR ( 'NONE', #106416, 1000.000000000000000 ) ;
#32458=ORIENTED_EDGE ( 'NONE', *, *, #74896, .F. ) ;
#32541=FACE_OUTER_BOUND ( 'NONE', #94514, .T. ) ;
#32557=CARTESIAN_POINT ( 'NONE',  ( -0.6250000000000004441, 8.299410119600873159, -7.298562697733108173 ) ) ;
#32589=VERTEX_POINT ( 'NONE', #6984 ) ;
#32633=EDGE_CURVE ( 'NONE', #20907, #82359, #8047, .T. ) ;
#32653=CARTESIAN_POINT ( 'NONE',  ( -4.250000000000000000, 5.204748896376250699E-16, -2.342872917771300578 ) ) ;
#32706=CARTESIAN_POINT ( 'NONE',  ( -7.500000000000000888, 0.000000000000000000, 1.734723475976807094E-15 ) ) ;
#32737=CARTESIAN_POINT ( 'NONE',  ( -1.843253007570911225E-16, -9.147862274876562338, -8.047472243342939535 ) ) ;
#32798=CARTESIAN_POINT ( 'NONE',  ( 0.000000000000000000, 0.000000000000000000, -5.710657142857142432 ) ) ;
#32805=CARTESIAN_POINT ( 'NONE',  ( -7.847095227763523084, -4.129731495738496960, -7.493596212620242447 ) ) ;
#32853=VERTEX_POINT ( 'NONE', #1956 ) ;
#32886=DIRECTION ( 'NONE',  ( -0.000000000000000000, -0.000000000000000000, -1.000000000000000000 ) ) ;
#32967=EDGE_CURVE ( 'NONE', #18381, #10075, #44720, .T. ) ;
#32992=DIRECTION ( 'NONE',  ( 0.000000000000000000, -0.000000000000000000, 1.000000000000000000 ) ) ;
#33050=CARTESIAN_POINT ( 'NONE',  ( -4.250000000000000000, 5.204748896376250699E-16, -0.5505556536572887572 ) ) ;
#33125=DIRECTION ( 'NONE',  ( -1.000000000000000000, 0.000000000000000000, 0.000000000000000000 ) ) ;
#33137=EDGE_LOOP ( 'NONE', ( #56889, #67668, #27814 ) ) ;
#33139=EDGE_CURVE ( 'NONE', #90336, #57292, #73456, .T. ) ;
#33145=PLANE ( 'NONE',  #5371 ) ;
#33151=CARTESIAN_POINT ( 'NONE',  ( -7.500000000000000000, -3.882691789159502971, -7.781695678276665973 ) ) ;
#33165=DIRECTION ( 'NONE',  ( 1.000000000000000000, 0.000000000000000000, 0.000000000000000000 ) ) ;
#33258=CARTESIAN_POINT ( 'NONE',  ( -6.602753909532903087, -5.319290460493550476, -7.792447862505339273 ) ) ;
#33316=CARTESIAN_POINT ( 'NONE',  ( -4.250000000000000000, 5.204748896376250699E-16, -10.00000000000000000 ) ) ;
#33327=LINE ( 'NONE', #96461, #104852 ) ;
#33337=AXIS2_PLACEMENT_3D ( 'NONE', #94339, #43644, #93799 ) ;
#33341=DIRECTION ( 'NONE',  ( -1.000000000000000000, 0.000000000000000000, 0.000000000000000000 ) ) ;
#33352=CARTESIAN_POINT ( 'NONE',  ( -6.486836893983013219, 4.915077010914094657, -7.231838333420560261 ) ) ;
#33469=DIRECTION ( 'NONE',  ( 1.000000000000000000, 0.000000000000000000, 0.000000000000000000 ) ) ;
#33481=CARTESIAN_POINT ( 'NONE',  ( -4.613983237546153582, 6.452243898629807184, -7.591546097228403234 ) ) ;
#33520=DIRECTION ( 'NONE',  ( 0.000000000000000000, 0.000000000000000000, 1.000000000000000000 ) ) ;
#33588=CIRCLE ( 'NONE', #90386, 5.000000000000000000 ) ;
#33610=CARTESIAN_POINT ( 'NONE',  ( -7.500000000000000000, 4.330127018922188320, -7.422398894150033399 ) ) ;
#33662=TOROIDAL_SURFACE ( 'NONE', #25046, 10.12668159690567826, 0.7733184030943209830 ) ;
#33673=FACE_OUTER_BOUND ( 'NONE', #52259, .T. ) ;
#33680=CARTESIAN_POINT ( 'NONE',  ( -7.500000000000000000, -3.105855721450334617, -7.659356991636312451 ) ) ;
#33740=CONICAL_SURFACE ( 'NONE', #47486, 5.000000000000000000, 0.9599310885968913576 ) ;
#33787=DIRECTION ( 'NONE',  ( 0.8191520442889884679, 0.000000000000000000, 0.5735764363510508224 ) ) ;
#33792=CARTESIAN_POINT ( 'NONE',  ( -7.922281120364393914, -4.573931137438282057, -8.047472243342934206 ) ) ;
#33828=DIRECTION ( 'NONE',  ( 0.000000000000000000, 0.000000000000000000, -1.000000000000000000 ) ) ;
#33892=CARTESIAN_POINT ( 'NONE',  ( -7.298354728638307698, 4.926141412640832051, -7.913704048100022703 ) ) ;
#33931=EDGE_LOOP ( 'NONE', ( #94351, #60635, #65397, #63388 ) ) ;
#33963=CARTESIAN_POINT ( 'NONE',  ( 0.000000000000000000, 0.000000000000000000, -2.868028571428571372 ) ) ;
#34113=VERTEX_POINT ( 'NONE', #57060 ) ;
#34147=ADVANCED_FACE ( 'NONE', ( #8515 ), #34460, .F. ) ;
#34167=CIRCLE ( 'NONE', #94450, 4.981862520314373377 ) ;
#34186=VERTEX_POINT ( 'NONE', #41418 ) ;
#34218=DIRECTION ( 'NONE',  ( -0.5000000000000006661, -0.8660254037844383745, 0.000000000000000000 ) ) ;
#34231=VECTOR ( 'NONE', #69376, 1000.000000000000000 ) ;
#34287=DIRECTION ( 'NONE',  ( -1.000000000000000000, 0.000000000000000000, 0.000000000000000000 ) ) ;
#34416=CARTESIAN_POINT ( 'NONE',  ( -6.658902113226989883, -5.287118297636340003, -7.776713651266857319 ) ) ;
#34421=CARTESIAN_POINT ( 'NONE',  ( 0.000000000000000000, 0.000000000000000000, -0.02540000000000007530 ) ) ;
#34436=CARTESIAN_POINT ( 'NONE',  ( -7.848314987057847247, 4.129027267381559341, -7.493854785173809319 ) ) ;
#34438=CARTESIAN_POINT ( 'NONE',  ( -7.894787914004607998, -1.231000152045941975E-13, -7.591390474663426424 ) ) ;
#34460=CONICAL_SURFACE ( 'NONE', #10314, 4.250000000000000000, 0.9599310885968754814 ) ;
#34483=DIRECTION ( 'NONE',  ( 0.000000000000000000, 0.000000000000000000, 1.000000000000000000 ) ) ;
#34708=AXIS2_PLACEMENT_3D ( 'NONE', #34421, #51616, #33341 ) ;
#34719=EDGE_LOOP ( 'NONE', ( #81273, #43158, #31734, #66335 ) ) ;
#34734=CARTESIAN_POINT ( 'NONE',  ( 10.12668159690567826, 0.000000000000000000, -9.226681596905679683 ) ) ;
#34754=CARTESIAN_POINT ( 'NONE',  ( -7.500000000000000000, -4.330127018922201643, -10.00000000000000000 ) ) ;
#34801=CARTESIAN_POINT ( 'NONE',  ( 2.503857664561936320E-16, -8.660254037844401509, -7.422398894150040505 ) ) ;
#34846=ORIENTED_EDGE ( 'NONE', *, *, #51035, .F. ) ;
#34876=DIRECTION ( 'NONE',  ( -0.8660254037844381525, -0.5000000000000008882, 0.000000000000000000 ) ) ;
#34940=CARTESIAN_POINT ( 'NONE',  ( -1.013163106017260562, -8.075304045852337964, -7.231838333420566478 ) ) ;
#34980=ORIENTED_EDGE ( 'NONE', *, *, #77900, .T. ) ;
#35101=COLOUR_RGB ( '', 0.08235294, 0.09019608, 0.10196078) ;
#35113=DIRECTION ( 'NONE',  ( -0.000000000000000000, -0.000000000000000000, -1.000000000000000000 ) ) ;
#35123=DIRECTION ( 'NONE',  ( -0.000000000000000000, -0.000000000000000000, -1.000000000000000000 ) ) ;
#35194=EDGE_LOOP ( 'NONE', ( #58342, #59192, #1748, #94174 ) ) ;
#35209=CYLINDRICAL_SURFACE ( 'NONE', #16482, 4.250000000000000000 ) ;
#35235=CARTESIAN_POINT ( 'NONE',  ( 0.000000000000000000, 0.000000000000000000, -8.553285714285713937 ) ) ;
#35348=LINE ( 'NONE', #76293, #13716 ) ;
#35373=CIRCLE ( 'NONE', #6074, 5.000000000000000888 ) ;
#35404=DIRECTION ( 'NONE',  ( -1.000000000000000000, 0.000000000000000000, 0.000000000000000000 ) ) ;
#35461=AXIS2_PLACEMENT_3D ( 'NONE', #1510, #17202, #84589 ) ;
#35477=CARTESIAN_POINT ( 'NONE',  ( -0.6169862416617590828, -8.783631307150894685, -7.913704048099813093 ) ) ;
#35645=ORIENTED_EDGE ( 'NONE', *, *, #32967, .T. ) ;
#35664=VERTEX_POINT ( 'NONE', #95584 ) ;
#35680=CARTESIAN_POINT ( 'NONE',  ( 0.000000000000000000, 0.000000000000000000, 1.734723475976807094E-15 ) ) ;
#35718=ADVANCED_FACE ( 'NONE', ( #4439 ), #30280, .F. ) ;
#35765=CIRCLE ( 'NONE', #101164, 4.250000000000000000 ) ;
#35813=CONICAL_SURFACE ( 'NONE', #80561, 4.250000000000000000, 0.9599310885968754814 ) ;
#35814=DIRECTION ( 'NONE',  ( -1.000000000000000000, 0.000000000000000000, 0.000000000000000000 ) ) ;
#35821=PLANE ( 'NONE',  #98092 ) ;
#35886=AXIS2_PLACEMENT_3D ( 'NONE', #33963, #41483, #91124 ) ;
#35937=AXIS2_PLACEMENT_3D ( 'NONE', #5416, #86881, #38339 ) ;
#35978=CIRCLE ( 'NONE', #56620, 4.250000000000000000 ) ;
#36012=ORIENTED_EDGE ( 'NONE', *, *, #62302, .T. ) ;
#36013=AXIS2_PLACEMENT_3D ( 'NONE', #87889, #86839, #46877 ) ;
#36034=AXIS2_PLACEMENT_3D ( 'NONE', #57296, #16319, #42189 ) ;
#36044=DIRECTION ( 'NONE',  ( 0.8191520442889975717, 1.003171929053531773E-16, -0.5735764363510378328 ) ) ;
#36070=DIRECTION ( 'NONE',  ( 0.000000000000000000, 0.000000000000000000, -1.000000000000000000 ) ) ;
#36093=LINE ( 'NONE', #77032, #90082 ) ;
#36103=CARTESIAN_POINT ( 'NONE',  ( -3.371112934716220631E-16, 8.660254037844390851, -7.564335161054499324 ) ) ;
#36196=AXIS2_PLACEMENT_3D ( 'NONE', #48729, #35123, #33125 ) ;
#36201=ORIENTED_EDGE ( 'NONE', *, *, #58152, .T. ) ;
#36204=CARTESIAN_POINT ( 'NONE',  ( -1.843253007570911225E-16, -9.147862274876562338, -8.047472243342939535 ) ) ;
#36384=CARTESIAN_POINT ( 'NONE',  ( -7.500000000000000000, -2.886751345948136205, -7.198902722707428481 ) ) ;
#36390=EDGE_CURVE ( 'NONE', #26814, #94271, #72101, .T. ) ;
#36407=ORIENTED_EDGE ( 'NONE', *, *, #58152, .F. ) ;
#36449=PRODUCT ( 'hex flange nut_din_Hexagon Flange Nut DIN 6923 - M10 - S', 'hex flange nut_din_Hexagon Flange Nut DIN 6923 - M10 - S', '', ( #20254 ) ) ;
#36478=B_SPLINE_CURVE_WITH_KNOTS ( 'NONE', 3,
 ( #94773, #93696, #77511, #94227, #10627, #20392 ),
 .UNSPECIFIED., .F., .F.,
 ( 4, 2, 4 ),
 ( -5.145455527296411814E-06, 0.0004153350442917297554, 0.0008358155441107577039 ),
 .UNSPECIFIED. ) ;
#36680=EDGE_LOOP ( 'NONE', ( #13833, #102207 ) ) ;
#36803=EDGE_LOOP ( 'NONE', ( #31482, #43873, #77051, #65981 ) ) ;
#36812=ORIENTED_EDGE ( 'NONE', *, *, #27673, .T. ) ;
#36823=DIRECTION ( 'NONE',  ( 0.000000000000000000, 0.000000000000000000, 1.000000000000000000 ) ) ;
#36828=CARTESIAN_POINT ( 'NONE',  ( 7.500000000000000000, -4.730916290271713009, -7.493595886788495086 ) ) ;
#36851=ORIENTED_EDGE ( 'NONE', *, *, #16736, .T. ) ;
#36871=B_SPLINE_CURVE_WITH_KNOTS ( 'NONE', 3,
 ( #32737, #15450, #74213, #65604, #292, #24642, #823, #33258, #66132, #33792 ),
 .UNSPECIFIED., .F., .F.,
 ( 4, 2, 2, 2, 4 ),
 ( 0.000000000000000000, 0.002305503304226491201, 0.004611006608452982401, 0.006916509912679473168, 0.009222013216905964803 ),
 .UNSPECIFIED. ) ;
#36874=DIRECTION ( 'NONE',  ( -1.000000000000000000, 0.000000000000000000, 0.000000000000000000 ) ) ;
#37064=LINE ( 'NONE', #85598, #46265 ) ;
#37091=LINE ( 'NONE', #61886, #98567 ) ;
#37102=DIRECTION ( 'NONE',  ( -1.000000000000000000, 0.000000000000000000, 0.000000000000000000 ) ) ;
#37103=ORIENTED_EDGE ( 'NONE', *, *, #101781, .T. ) ;
#37187=ORIENTED_EDGE ( 'NONE', *, *, #67199, .T. ) ;
#37226=CARTESIAN_POINT ( 'NONE',  ( 4.250000000000000000, 0.000000000000000000, -7.657127082228716297 ) ) ;
#37257=VERTEX_POINT ( 'NONE', #104072 ) ;
#37296=CONICAL_SURFACE ( 'NONE', #80274, 7.500000000000000888, 0.8594454914424817238 ) ;
#37343=FILL_AREA_STYLE_COLOUR ( '', #35101 ) ;
#37398=EDGE_LOOP ( 'NONE', ( #53412, #23496, #46157, #20704 ) ) ;
#37532=VECTOR ( 'NONE', #26624, 1000.000000000000000 ) ;
#37657=DIRECTION ( 'NONE',  ( -1.000000000000000000, 0.000000000000000000, 0.000000000000000000 ) ) ;
#37669=B_SPLINE_CURVE_WITH_KNOTS ( 'NONE', 3,
 ( #76127, #93918, #77740, #51850, #43763, #11921, #85847, #18455, #52379 ),
 .UNSPECIFIED., .F., .F.,
 ( 4, 2, 1, 2, 4 ),
 ( 0.000000000000000000, 0.002165063509461097498, 0.004330127018922194995, 0.006495190528383292493, 0.008660254037844389990 ),
 .UNSPECIFIED. ) ;
#37687=VECTOR ( 'NONE', #14188, 1000.000000000000000 ) ;
#37852=DIRECTION ( 'NONE',  ( -0.000000000000000000, -0.000000000000000000, -1.000000000000000000 ) ) ;
#37869=CARTESIAN_POINT ( 'NONE',  ( -4.250000000000000000, 5.204748896376250699E-16, -3.393184225085859929 ) ) ;
#37914=CIRCLE ( 'NONE', #99923, 5.000000000000000000 ) ;
#37962=CARTESIAN_POINT ( 'NONE',  ( 7.263825692932301514, 4.945657111639576442, -7.907570769506051533 ) ) ;
#37968=ORIENTED_EDGE ( 'NONE', *, *, #61429, .T. ) ;
#38031=FACE_BOUND ( 'NONE', #36680, .T. ) ;
#38110=DIRECTION ( 'NONE',  ( 0.000000000000000000, 0.000000000000000000, -1.000000000000000000 ) ) ;
#38136=CONICAL_SURFACE ( 'NONE', #39798, 5.000000000000000000, 0.9599310885968913576 ) ;
#38154=DIRECTION ( 'NONE',  ( 0.5000000000000008882, 0.8660254037844382635, -0.000000000000000000 ) ) ;
#38185=ORIENTED_EDGE ( 'NONE', *, *, #30875, .T. ) ;
#38191=ORIENTED_EDGE ( 'NONE', *, *, #525, .F. ) ;
#38245=LINE ( 'NONE', #46829, #48758 ) ;
#38290=EDGE_CURVE ( 'NONE', #26814, #95526, #90853, .T. ) ;
#38339=DIRECTION ( 'NONE',  ( -1.000000000000000000, 0.000000000000000000, 0.000000000000000000 ) ) ;
#38430=CARTESIAN_POINT ( 'NONE',  ( 0.000000000000000000, 0.000000000000000000, -4.289342857142857568 ) ) ;
#38530=VERTEX_POINT ( 'NONE', #67652 ) ;
#38565=CARTESIAN_POINT ( 'NONE',  ( -3.093157300003891219, -6.874418838041296276, -7.169286865560398070E-15 ) ) ;
#38576=CARTESIAN_POINT ( 'NONE',  ( 7.500000000000000000, 1.489914625144004523, -0.1187923833806734525 ) ) ;
#38637=DIRECTION ( 'NONE',  ( 1.000000000000000000, 0.000000000000000000, 0.000000000000000000 ) ) ;
#38736=DIRECTION ( 'NONE',  ( 0.000000000000000000, 0.000000000000000000, 1.000000000000000000 ) ) ;
#38783=CARTESIAN_POINT ( 'NONE',  ( -0.9763930676160361699, 8.096533237421388307, -7.213065638943060520 ) ) ;
#38807=EDGE_LOOP ( 'NONE', ( #6940, #77248, #54053, #67166, #15437 ) ) ;
#38920=CARTESIAN_POINT ( 'NONE',  ( 7.894705354778059458, 0.7527931906213466418, -7.590204373988306941 ) ) ;
#38927=DIRECTION ( 'NONE',  ( 0.000000000000000000, 0.000000000000000000, 1.000000000000000000 ) ) ;
#38975=DIRECTION ( 'NONE',  ( -0.8191520442889975717, 0.000000000000000000, -0.5735764363510378328 ) ) ;
#39029=EDGE_CURVE ( 'NONE', #27490, #103169, #105343, .T. ) ;
#39215=CARTESIAN_POINT ( 'NONE',  ( 0.000000000000000000, 0.000000000000000000, 0.000000000000000000 ) ) ;
#39278=DIRECTION ( 'NONE',  ( -0.000000000000000000, -0.000000000000000000, 1.000000000000000000 ) ) ;
#39285=FACE_OUTER_BOUND ( 'NONE', #19483, .T. ) ;
#39287=DIRECTION ( 'NONE',  ( 0.000000000000000000, 0.000000000000000000, 1.000000000000000000 ) ) ;
#39338=CARTESIAN_POINT ( 'NONE',  ( 3.295171437449430307, 7.213553046161576887, -7.590212325761433121 ) ) ;
#39354=ORIENTED_EDGE ( 'NONE', *, *, #96453, .F. ) ;
#39430=CARTESIAN_POINT ( 'NONE',  ( 7.914984360234579519, -3.818534719232097085, -7.907701344400645205 ) ) ;
#39464=DIRECTION ( 'NONE',  ( 1.000000000000000000, 0.000000000000000000, 0.000000000000000000 ) ) ;
#39483=CARTESIAN_POINT ( 'NONE',  ( 0.000000000000000000, 0.000000000000000000, -10.00000000000000000 ) ) ;
#39506=CARTESIAN_POINT ( 'NONE',  ( -7.908030677224553884, 3.059924800338339246, -7.792662696733363425 ) ) ;
#39537=CONICAL_SURFACE ( 'NONE', #22380, 5.000000000000000000, 0.9599310885968913576 ) ;
#39597=EDGE_LOOP ( 'NONE', ( #29132, #68688, #56219, #71480 ) ) ;
#39649=CARTESIAN_POINT ( 'NONE',  ( -7.500000000000000000, -1.572902445675619099, -7.069816568113129307 ) ) ;
#39749=ORIENTED_EDGE ( 'NONE', *, *, #78052, .T. ) ;
#39798=AXIS2_PLACEMENT_3D ( 'NONE', #105417, #70406, #46131 ) ;
#39817=CARTESIAN_POINT ( 'NONE',  ( -4.250000000000000000, 5.204748896376250699E-16, -9.078441367943003826 ) ) ;
#39863=AXIS2_PLACEMENT_3D ( 'NONE', #12367, #43159, #45292 ) ;
#40015=ORIENTED_EDGE ( 'NONE', *, *, #49242, .T. ) ;
#40147=CARTESIAN_POINT ( 'NONE',  ( 4.599534470798633201, -6.460478697736662390, -7.590212325761506840 ) ) ;
#40174=CARTESIAN_POINT ( 'NONE',  ( 7.500000000000002665, -1.486698507076798625, -0.09861472150523793723 ) ) ;
#40205=SURFACE_STYLE_USAGE ( .BOTH. , #97908 ) ;
#40235=B_SPLINE_CURVE_WITH_KNOTS ( 'NONE', 3,
 ( #26087, #92348, #50818, #60550, #43809, #28205 ),
 .UNSPECIFIED., .F., .F.,
 ( 4, 2, 4 ),
 ( -5.145455527292617106E-06, 0.0004153350442917344717, 0.0008358155441107594386 ),
 .UNSPECIFIED. ) ;
#40416=ORIENTED_EDGE ( 'NONE', *, *, #69682, .T. ) ;
#40437=ORIENTED_EDGE ( 'NONE', *, *, #91657, .F. ) ;
#40479=AXIS2_PLACEMENT_3D ( 'NONE', #27633, #93398, #85295 ) ;
#40502=ORIENTED_EDGE ( 'NONE', *, *, #63592, .T. ) ;
#40672=DIRECTION ( 'NONE',  ( 0.000000000000000000, 0.000000000000000000, 1.000000000000000000 ) ) ;
#40750=AXIS2_PLACEMENT_3D ( 'NONE', #17754, #32886, #106193 ) ;
#40757=EDGE_CURVE ( 'NONE', #75037, #27550, #29158, .T. ) ;
#40802=ADVANCED_FACE ( 'NONE', ( #79770 ), #31629, .F. ) ;
#40844=B_SPLINE_CURVE_WITH_KNOTS ( 'NONE', 3,
 ( #106395, #32557, #26081, #91832, #41681, #73496, #1738, #58940, #33610 ),
 .UNSPECIFIED., .F., .F.,
 ( 4, 2, 1, 2, 4 ),
 ( 0.000000000000000000, 0.002165063509461097931, 0.004330127018922195863, 0.006495190528383293360, 0.008660254037844391725 ),
 .UNSPECIFIED. ) ;
#40855=CARTESIAN_POINT ( 'NONE',  ( -5.000000000000000000, 0.000000000000000000, -8.553285714285713937 ) ) ;
#40914=DIRECTION ( 'NONE',  ( 0.000000000000000000, 0.000000000000000000, 1.000000000000000000 ) ) ;
#40958=EDGE_CURVE ( 'NONE', #103169, #91741, #74734, .T. ) ;
#41063=LINE ( 'NONE', #56697, #73841 ) ;
#41210=CARTESIAN_POINT ( 'NONE',  ( 1.249327701957322123, -8.410337540183546068, -7.776713651265729332 ) ) ;
#41286=EDGE_CURVE ( 'NONE', #13350, #20962, #4925, .T. ) ;
#41372=ORIENTED_EDGE ( 'NONE', *, *, #77485, .T. ) ;
#41392=FACE_OUTER_BOUND ( 'NONE', #101398, .T. ) ;
#41418=CARTESIAN_POINT ( 'NONE',  ( 4.250000000000000000, 0.000000000000000000, -8.028130060628445364 ) ) ;
#41483=DIRECTION ( 'NONE',  ( -0.000000000000000000, -0.000000000000000000, -1.000000000000000000 ) ) ;
#41508=ADVANCED_FACE ( 'NONE', ( #10155 ), #51673, .F. ) ;
#41535=FACE_OUTER_BOUND ( 'NONE', #20352, .T. ) ;
#41559=CARTESIAN_POINT ( 'NONE',  ( 7.500000000000000000, 3.160172554975069215, -7.231829826456838362 ) ) ;
#41574=LINE ( 'NONE', #2160, #72489 ) ;
#41681=CARTESIAN_POINT ( 'NONE',  ( -3.750000000000002665, 6.495190528383289141, -6.991905250253755533 ) ) ;
#41739=CARTESIAN_POINT ( 'NONE',  ( 5.276498195232712796, -6.073236878018009044, -7.633618187056885773 ) ) ;
#41753=EDGE_LOOP ( 'NONE', ( #17458, #75452, #48197, #45925 ) ) ;
#41759=CARTESIAN_POINT ( 'NONE',  ( 0.000000000000000000, 0.000000000000000000, -9.974599999999998801 ) ) ;
#41903=CARTESIAN_POINT ( 'NONE',  ( 0.000000000000000000, 0.000000000000000000, -9.078441367943003826 ) ) ;
#41929=CARTESIAN_POINT ( 'NONE',  ( -7.968863443239236233, -4.547634245050486079, -8.057411785091790790 ) ) ;
#41958=AXIS2_PLACEMENT_3D ( 'NONE', #4184, #94808, #37657 ) ;
#41978=B_SPLINE_CURVE_WITH_KNOTS ( 'NONE', 3,
 ( #59121, #1916, #92004, #17603, #68815, #18685 ),
 .UNSPECIFIED., .F., .F.,
 ( 4, 2, 4 ),
 ( 2.475503369199568371E-07, 0.002222330217055625001, 0.004444412883774330643 ),
 .UNSPECIFIED. ) ;
#41993=DIRECTION ( 'NONE',  ( 1.000000000000000000, 0.000000000000000000, 0.000000000000000000 ) ) ;
#42061=EDGE_LOOP ( 'NONE', ( #61794, #88, #105406, #52217 ) ) ;
#42189=DIRECTION ( 'NONE',  ( 1.000000000000000000, 0.000000000000000000, 0.000000000000000000 ) ) ;
#42258=ORIENTED_EDGE ( 'NONE', *, *, #95099, .T. ) ;
#42362=DIRECTION ( 'NONE',  ( 0.000000000000000000, 0.000000000000000000, -1.000000000000000000 ) ) ;
#42436=AXIS2_PLACEMENT_3D ( 'NONE', #64213, #22706, #87949 ) ;
#42459=CARTESIAN_POINT ( 'NONE',  ( -3.080866544137897289, -6.881514909249071721, -7.026396753507436976 ) ) ;
#42478=CARTESIAN_POINT ( 'NONE',  ( -7.779103221381271638, 4.168986698926019585, -7.929128246061903695 ) ) ;
#42480=DIRECTION ( 'NONE',  ( 1.000000000000000000, 0.000000000000000000, 0.000000000000000000 ) ) ;
#42507=EDGE_CURVE ( 'NONE', #23008, #4416, #106476, .T. ) ;
#42540=CARTESIAN_POINT ( 'NONE',  ( 1.688352148327314640E-15, 8.895721644649736248, -7.917989418073286600 ) ) ;
#42577=DIRECTION ( 'NONE',  ( -0.000000000000000000, -0.000000000000000000, -1.000000000000000000 ) ) ;
#42585=AXIS2_PLACEMENT_3D ( 'NONE', #63816, #31465, #104787 ) ;
#42699=DIRECTION ( 'NONE',  ( -1.000000000000000000, 0.000000000000000000, 0.000000000000000000 ) ) ;
#42721=CARTESIAN_POINT ( 'NONE',  ( -6.902527771671634227, -4.675077770780910136, -0.7026937717022843088 ) ) ;
#42810=EDGE_CURVE ( 'NONE', #2343, #54954, #986, .T. ) ;
#42877=DIRECTION ( 'NONE',  ( -0.000000000000000000, -0.000000000000000000, -1.000000000000000000 ) ) ;
#42955=ORIENTED_EDGE ( 'NONE', *, *, #3608, .T. ) ;
#42970=CARTESIAN_POINT ( 'NONE',  ( 1.249999999999999556, 7.938566201357357244, -7.198902722707429369 ) ) ;
#43013=AXIS2_PLACEMENT_3D ( 'NONE', #94870, #87831, #64096 ) ;
#43071=VECTOR ( 'NONE', #104826, 1000.000000000000000 ) ;
#43100=CIRCLE ( 'NONE', #58578, 4.250000000000000000 ) ;
#43121=ORIENTED_EDGE ( 'NONE', *, *, #18809, .F. ) ;
#43158=ORIENTED_EDGE ( 'NONE', *, *, #2580, .T. ) ;
#43159=DIRECTION ( 'NONE',  ( -0.000000000000000000, -0.000000000000000000, -1.000000000000000000 ) ) ;
#43187=CARTESIAN_POINT ( 'NONE',  ( 2.920238372941035660E-16, -8.660254037844401509, -7.564338275809348033 ) ) ;
#43202=DIRECTION ( 'NONE',  ( -0.000000000000000000, -0.000000000000000000, 1.000000000000000000 ) ) ;
#43266=EDGE_CURVE ( 'NONE', #57728, #52946, #51435, .T. ) ;
#43297=AXIS2_PLACEMENT_3D ( 'NONE', #45268, #45784, #61457 ) ;
#43483=PRODUCT_DEFINITION_CONTEXT ( 'detailed design', #100339, 'design' ) ;
#43552=CARTESIAN_POINT ( 'NONE',  ( -6.439685834476830628, 4.942299687813059172, -7.659344964963183955 ) ) ;
#43592=DIRECTION ( 'NONE',  ( 1.000000000000000000, 0.000000000000000000, 0.000000000000000000 ) ) ;
#43642=DIRECTION ( 'NONE',  ( -1.000000000000000000, 0.000000000000000000, 0.000000000000000000 ) ) ;
#43644=DIRECTION ( 'NONE',  ( -0.000000000000000000, -0.000000000000000000, -1.000000000000000000 ) ) ;
#43654=ORIENTED_EDGE ( 'NONE', *, *, #74327, .T. ) ;
#43684=CIRCLE ( 'NONE', #4047, 4.250000000000000000 ) ;
#43699=CARTESIAN_POINT ( 'NONE',  ( 2.623433461001182909, -7.604994000793868558, -7.633824513837120129 ) ) ;
#43763=CARTESIAN_POINT ( 'NONE',  ( 7.500000000000000000, -6.938893903907228378E-15, -6.991905250253755533 ) ) ;
#43781=CARTESIAN_POINT ( 'NONE',  ( -6.288404560131954923, -5.029641972278941608, -0.4504974108211988182 ) ) ;
#43788=FACE_OUTER_BOUND ( 'NONE', #65736, .T. ) ;
#43809=CARTESIAN_POINT ( 'NONE',  ( -7.500000000000000000, -4.330127018922200755, -7.564335161054497547 ) ) ;
#43868=FACE_OUTER_BOUND ( 'NONE', #38807, .T. ) ;
#43873=ORIENTED_EDGE ( 'NONE', *, *, #33139, .T. ) ;
#43892=DIRECTION ( 'NONE',  ( 1.000000000000000000, 0.000000000000000000, 0.000000000000000000 ) ) ;
#43912=ADVANCED_FACE ( 'NONE', ( #71270 ), #24704, .F. ) ;
#43993=DIRECTION ( 'NONE',  ( -0.000000000000000000, -0.000000000000000000, -1.000000000000000000 ) ) ;
#44083=CARTESIAN_POINT ( 'NONE',  ( -7.500000000000000000, -4.330127018922201643, -7.422398894150036064 ) ) ;
#44124=ORIENTED_EDGE ( 'NONE', *, *, #42810, .F. ) ;
#44185=CONICAL_SURFACE ( 'NONE', #20126, 4.250000000000000000, 0.9599310885968754814 ) ;
#44351=AXIS2_PLACEMENT_3D ( 'NONE', #55800, #89270, #80623 ) ;
#44430=AXIS2_PLACEMENT_3D ( 'NONE', #28494, #36070, #19888 ) ;
#44610=CARTESIAN_POINT ( 'NONE',  ( 0.3483149870578539087, -8.861353789385034929, -7.493854785173817312 ) ) ;
#44641=CONICAL_SURFACE ( 'NONE', #43013, 5.000000000000000000, 0.9599310885968913576 ) ;
#44720=B_SPLINE_CURVE_WITH_KNOTS ( 'NONE', 3,
 ( #58628, #17642, #94037, #50503, #83415, #7926, #42970, #9514, #51037 ),
 .UNSPECIFIED., .F., .F.,
 ( 4, 2, 1, 2, 4 ),
 ( 0.000000000000000000, 0.002165063509461097931, 0.004330127018922195863, 0.006495190528383293360, 0.008660254037844391725 ),
 .UNSPECIFIED. ) ;
#44767=ORIENTED_EDGE ( 'NONE', *, *, #61429, .F. ) ;
#44833=ADVANCED_BREP_SHAPE_REPRESENTATION ( '', ( #17528, #10728 ), #71253 ) ;
#44862=CARTESIAN_POINT ( 'NONE',  ( -5.000000000000000000, 0.000000000000000000, -0.02540000000000007530 ) ) ;
#44884=VERTEX_POINT ( 'NONE', #45311 ) ;
#44885=( LENGTH_UNIT ( ) NAMED_UNIT ( * ) SI_UNIT ( .MILLI., .METRE. ) );
#44892=CIRCLE ( 'NONE', #26064, 10.39117206796836257 ) ;
#44967=ORIENTED_EDGE ( 'NONE', *, *, #69469, .T. ) ;
#44999=EDGE_CURVE ( 'NONE', #106581, #4153, #65208, .T. ) ;
#45019=CONICAL_SURFACE ( 'NONE', #34708, 5.000000000000000000, 0.9599310885968913576 ) ;
#45026=SHAPE_DEFINITION_REPRESENTATION ( #60525, #7490 ) ;
#45076=ORIENTED_EDGE ( 'NONE', *, *, #97150, .T. ) ;
#45145=CARTESIAN_POINT ( 'NONE',  ( 10.39117206796836435, 0.000000000000000000, -8.500000000000000000 ) ) ;
#45257=DIRECTION ( 'NONE',  ( 1.000000000000000000, 0.000000000000000000, 0.000000000000000000 ) ) ;
#45268=CARTESIAN_POINT ( 'NONE',  ( 0.000000000000000000, 0.000000000000000000, -0.5505556536572887572 ) ) ;
#45273=ORIENTED_EDGE ( 'NONE', *, *, #62302, .F. ) ;
#45292=DIRECTION ( 'NONE',  ( -1.000000000000000000, 0.000000000000000000, 0.000000000000000000 ) ) ;
#45311=CARTESIAN_POINT ( 'NONE',  ( 7.500000000000000888, 0.000000000000000000, 1.734723475976807094E-15 ) ) ;
#45380=VERTEX_POINT ( 'NONE', #105526 ) ;
#45559=CARTESIAN_POINT ( 'NONE',  ( 0.000000000000000000, 0.000000000000000000, -10.00000000000000000 ) ) ;
#45664=CARTESIAN_POINT ( 'NONE',  ( -1.282512619719470059, -8.391164935524027868, -7.795653906408888112 ) ) ;
#45784=DIRECTION ( 'NONE',  ( 0.000000000000000000, 0.000000000000000000, 1.000000000000000000 ) ) ;
#45819=EDGE_CURVE ( 'NONE', #26769, #57292, #102222, .T. ) ;
#45925=ORIENTED_EDGE ( 'NONE', *, *, #40958, .F. ) ;
#45949=LINE ( 'NONE', #55074, #29202 ) ;
#45978=DIRECTION ( 'NONE',  ( -1.000000000000000000, 0.000000000000000000, 0.000000000000000000 ) ) ;
#46005=AXIS2_PLACEMENT_3D ( 'NONE', #103220, #54632, #46567 ) ;
#46113=AXIS2_PLACEMENT_3D ( 'NONE', #18676, #2447, #1366 ) ;
#46116=CARTESIAN_POINT ( 'NONE',  ( -1.908195823574487804E-14, -8.660254037844390851, -0.9999999999999974465 ) ) ;
#46131=DIRECTION ( 'NONE',  ( -1.000000000000000000, 0.000000000000000000, 0.000000000000000000 ) ) ;
#46157=ORIENTED_EDGE ( 'NONE', *, *, #96453, .T. ) ;
#46174=CIRCLE ( 'NONE', #35886, 5.000000000000000000 ) ;
#46192=AXIS2_PLACEMENT_3D ( 'NONE', #8559, #34483, #41993 ) ;
#46239=ORIENTED_EDGE ( 'NONE', *, *, #3671, .T. ) ;
#46265=VECTOR ( 'NONE', #62384, 1000.000000000000000 ) ;
#46304=CARTESIAN_POINT ( 'NONE',  ( 7.549006887134069643, 4.358421158401191597, -7.700127545397313256 ) ) ;
#46317=EDGE_CURVE ( 'NONE', #71702, #22401, #37914, .T. ) ;
#46372=ORIENTED_EDGE ( 'NONE', *, *, #56286, .F. ) ;
#46471=CONICAL_SURFACE ( 'NONE', #99811, 5.000000000000000000, 0.9599310885968913576 ) ;
#46480=FACE_OUTER_BOUND ( 'NONE', #48913, .T. ) ;
#46506=ORIENTED_EDGE ( 'NONE', *, *, #99922, .T. ) ;
#46567=DIRECTION ( 'NONE',  ( -1.000000000000000000, 0.000000000000000000, 0.000000000000000000 ) ) ;
#46656=ORIENTED_EDGE ( 'NONE', *, *, #53366, .F. ) ;
#46670=CARTESIAN_POINT ( 'NONE',  ( -7.499999999999999112, 0.3744244963005058935, 2.466559942404519826E-15 ) ) ;
#46726=CARTESIAN_POINT ( 'NONE',  ( 0.000000000000000000, 0.000000000000000000, -9.078441367943003826 ) ) ;
#46829=CARTESIAN_POINT ( 'NONE',  ( 4.250000000000000000, 0.000000000000000000, -10.00000000000000000 ) ) ;
#46855=CARTESIAN_POINT ( 'NONE',  ( 1.211595439868047741, -7.960739084487659767, -0.4504974108212048689 ) ) ;
#46871=CARTESIAN_POINT ( 'NONE',  ( 1.013163106017262338, 8.075304045852325530, -7.231838333420562037 ) ) ;
#46877=DIRECTION ( 'NONE',  ( -1.000000000000000000, 0.000000000000000000, 0.000000000000000000 ) ) ;
#46887=ORIENTED_EDGE ( 'NONE', *, *, #48393, .F. ) ;
#46896=DIRECTION ( 'NONE',  ( -1.000000000000000000, 0.000000000000000000, 0.000000000000000000 ) ) ;
#46912=B_SPLINE_CURVE_WITH_KNOTS ( 'NONE', 3,
 ( #5316, #5828, #46304, #79193, #103989, #30135 ),
 .UNSPECIFIED., .F., .F.,
 ( 4, 2, 4 ),
 ( 0.000000000000000000, 0.0004189869898914146498, 0.0008379739797828311427 ),
 .UNSPECIFIED. ) ;
#46919=CIRCLE ( 'NONE', #55522, 4.250000000000000000 ) ;
#46975=( NAMED_UNIT ( * ) SI_UNIT ( $, .STERADIAN. ) SOLID_ANGLE_UNIT ( ) );
#46993=ORIENTED_EDGE ( 'NONE', *, *, #39029, .F. ) ;
#47010=( BOUNDED_SURFACE ( )  B_SPLINE_SURFACE ( 3, 2, ( 
 ( #23468, #57910, #83259 ),
 ( #97849, #57379, #41210 ),
 ( #90293, #16402, #74096 ),
 ( #75156, #16950, #40147 ),
 ( #56851, #97316, #41739 ),
 ( #74626, #49828, #81643 ),
 ( #89244, #25605, #49285 ),
 ( #73025, #82188, #15342 ) ),
 .UNSPECIFIED., .F., .F., .F. ) 
 B_SPLINE_SURFACE_WITH_KNOTS ( ( 4, 2, 2, 4 ),
 ( 3, 3 ),
 ( 0.03861844051980971304, 0.04325213341840643266, 0.04556897986770479247, 0.04788582631700314535 ),
 ( 0.000000000000000000, 1.000000000000000000 ),
 .UNSPECIFIED. ) 
 GEOMETRIC_REPRESENTATION_ITEM ( )  RATIONAL_B_SPLINE_SURFACE ( (
 ( 1.000000000000000000, 0.8047781759831919013, 1.000000000000000000),
 ( 1.000000000000000000, 0.8123762462805835805, 1.000000000000000000),
 ( 1.000000000000000000, 0.8190659850615710225, 1.000000000000000000),
 ( 1.000000000000000000, 0.8191937571014150654, 1.000000000000000000),
 ( 1.000000000000000000, 0.8176092952781637280, 1.000000000000000000),
 ( 1.000000000000000000, 0.8122962088595298003, 1.000000000000000000),
 ( 1.000000000000000000, 0.8086311330828849231, 1.000000000000000000),
 ( 1.000000000000000000, 0.8047712282214323221, 1.000000000000000000) ) ) 
 REPRESENTATION_ITEM ( '' )  SURFACE ( )  );
#47066=AXIS2_PLACEMENT_3D ( 'NONE', #18761, #74289, #18216 ) ;
#47110=ADVANCED_FACE ( 'NONE', ( #57131 ), #82487, .F. ) ;
#47124=DIRECTION ( 'NONE',  ( -0.000000000000000000, -0.000000000000000000, -1.000000000000000000 ) ) ;
#47140=STYLED_ITEM ( 'NONE', ( #104408 ), #17528 ) ;
#47225=B_SPLINE_CURVE_WITH_KNOTS ( 'NONE', 3,
 ( #80096, #95245, #89269, #13765, #5168, #40174, #63422, #56337 ),
 .UNSPECIFIED., .F., .F.,
 ( 4, 2, 2, 4 ),
 ( 0.006061689441712474202, 0.007174127271521698983, 0.008286565101330923763, 0.01051144076094937159 ),
 .UNSPECIFIED. ) ;
#47243=ORIENTED_EDGE ( 'NONE', *, *, #103079, .T. ) ;
#47259=VECTOR ( 'NONE', #12551, 1000.000000000000000 ) ;
#47295=PRODUCT_DEFINITION_FORMATION_WITH_SPECIFIED_SOURCE ( 'ANY', '', #36449, .NOT_KNOWN. ) ;
#47312=DIRECTION ( 'NONE',  ( -0.000000000000000000, -0.000000000000000000, -1.000000000000000000 ) ) ;
#47349=FACE_OUTER_BOUND ( 'NONE', #4762, .T. ) ;
#47397=CARTESIAN_POINT ( 'NONE',  ( 3.093533885182577325, 6.874201416486802607, -7.446478553994766436 ) ) ;
#47486=AXIS2_PLACEMENT_3D ( 'NONE', #19291, #100141, #92051 ) ;
#47487=AXIS2_PLACEMENT_3D ( 'NONE', #78080, #93740, #12273 ) ;
#47693=CARTESIAN_POINT ( 'NONE',  ( 7.500000000000000000, 4.330127018922203419, -0.9999999999999974465 ) ) ;
#47701=CARTESIAN_POINT ( 'NONE',  ( -7.500000000000000000, 3.202583086481786356, -7.213046687578396288 ) ) ;
#47727=CARTESIAN_POINT ( 'NONE',  ( 0.000000000000000000, 0.000000000000000000, 0.000000000000000000 ) ) ;
#47742=FACE_OUTER_BOUND ( 'NONE', #28280, .T. ) ;
#47873=CARTESIAN_POINT ( 'NONE',  ( 0.000000000000000000, 0.000000000000000000, -2.868028571428571372 ) ) ;
#47878=DIRECTION ( 'NONE',  ( 1.000000000000000000, 0.000000000000000000, 0.000000000000000000 ) ) ;
#47891=EDGE_LOOP ( 'NONE', ( #95218, #61536, #78308, #88703 ) ) ;
#47973=EDGE_CURVE ( 'NONE', #44884, #37257, #69160, .T. ) ;
#48037=AXIS2_PLACEMENT_3D ( 'NONE', #69356, #19252, #34876 ) ;
#48039=CARTESIAN_POINT ( 'NONE',  ( -4.250000000000000000, 5.204748896376250699E-16, -10.00000000000000000 ) ) ;
#48040=CARTESIAN_POINT ( 'NONE',  ( 7.897825807688775512, 1.532833846124507238, -7.633607627188419897 ) ) ;
#48197=ORIENTED_EDGE ( 'NONE', *, *, #94907, .F. ) ;
#48199=AXIS2_PLACEMENT_3D ( 'NONE', #65637, #33828, #99583 ) ;
#48224=CARTESIAN_POINT ( 'NONE',  ( 0.000000000000000000, 0.000000000000000000, -6.235812796514431433 ) ) ;
#48316=DIRECTION ( 'NONE',  ( -1.000000000000000000, 0.000000000000000000, 0.000000000000000000 ) ) ;
#48353=CARTESIAN_POINT ( 'NONE',  ( -5.000000000000000000, 0.000000000000000000, -9.974599999999998801 ) ) ;
#48393=EDGE_CURVE ( 'NONE', #93010, #53023, #92557, .T. ) ;
#48423=VERTEX_POINT ( 'NONE', #30937 ) ;
#48437=CARTESIAN_POINT ( 'NONE',  ( -1.015826369456739098, 8.073766409989460158, -7.642786413615525909 ) ) ;
#48461=CIRCLE ( 'NONE', #63985, 7.500000000000003553 ) ;
#48621=CARTESIAN_POINT ( 'NONE',  ( -7.897850199329715437, 1.533397866934074427, -7.634054012537970557 ) ) ;
#48708=ORIENTED_EDGE ( 'NONE', *, *, #19561, .F. ) ;
#48729=CARTESIAN_POINT ( 'NONE',  ( 0.000000000000000000, 0.000000000000000000, -8.553285714285713937 ) ) ;
#48734=DIRECTION ( 'NONE',  ( -0.000000000000000000, -0.000000000000000000, -1.000000000000000000 ) ) ;
#48758=VECTOR ( 'NONE', #29627, 1000.000000000000000 ) ;
#48774=CARTESIAN_POINT ( 'NONE',  ( -7.500000000000001776, 2.932633423934438710, -0.4709827563909262937 ) ) ;
#48786=FACE_OUTER_BOUND ( 'NONE', #73983, .T. ) ;
#48798=CARTESIAN_POINT ( 'NONE',  ( 0.000000000000000000, 0.000000000000000000, -10.00000000000000000 ) ) ;
#48805=ORIENTED_EDGE ( 'NONE', *, *, #77588, .F. ) ;
#48863=ORIENTED_EDGE ( 'NONE', *, *, #6280, .T. ) ;
#48876=ORIENTED_EDGE ( 'NONE', *, *, #39029, .T. ) ;
#48913=EDGE_LOOP ( 'NONE', ( #103519, #98246, #61324, #98272 ) ) ;
#48958=CARTESIAN_POINT ( 'NONE',  ( -3.750000000000007105, 6.495190528383286477, 1.734723475976807094E-15 ) ) ;
#48972=CARTESIAN_POINT ( 'NONE',  ( 7.922281120364393914, -4.573931137438281169, -8.047472243342934206 ) ) ;
#48973=ADVANCED_FACE ( 'NONE', ( #83941 ), #62026, .T. ) ;
#48980=ORIENTED_EDGE ( 'NONE', *, *, #9885, .F. ) ;
#49023=EDGE_LOOP ( 'NONE', ( #45076, #22676, #23795, #79154, #37968, #65318, #104007 ) ) ;
#49138=ADVANCED_FACE ( 'NONE', ( #70430 ), #72318, .F. ) ;
#49242=EDGE_CURVE ( 'NONE', #84586, #72526, #67255, .T. ) ;
#49245=DIRECTION ( 'NONE',  ( -0.000000000000000000, -0.000000000000000000, 1.000000000000000000 ) ) ;
#49285=CARTESIAN_POINT ( 'NONE',  ( 7.298354728638322797, -4.926141412640330230, -7.913704048099935662 ) ) ;
#49288=CARTESIAN_POINT ( 'NONE',  ( -7.499999999999999112, 1.613867362011851325, -7.450195926347907616 ) ) ;
#49294=ORIENTED_EDGE ( 'NONE', *, *, #5978, .F. ) ;
#49331=DIRECTION ( 'NONE',  ( -1.000000000000000000, 0.000000000000000000, 0.000000000000000000 ) ) ;
#49340=VERTEX_POINT ( 'NONE', #83281 ) ;
#49372=CARTESIAN_POINT ( 'NONE',  ( -7.500000000000000888, -0.7512838658081425480, 2.510605655661746205E-15 ) ) ;
#49404=VECTOR ( 'NONE', #36044, 1000.000000000000000 ) ;
#49539=ORIENTED_EDGE ( 'NONE', *, *, #78440, .T. ) ;
#49748=ORIENTED_EDGE ( 'NONE', *, *, #71487, .F. ) ;
#49796=ORIENTED_EDGE ( 'NONE', *, *, #53898, .F. ) ;
#49828=CARTESIAN_POINT ( 'NONE',  ( 6.439685834476087223, -4.942299687812549358, -7.659344964962875757 ) ) ;
#49900=CARTESIAN_POINT ( 'NONE',  ( 4.999999999999998224, -5.773502691896267969, -7.063244554130005071 ) ) ;
#49917=CARTESIAN_POINT ( 'NONE',  ( 0.000000000000000000, 0.000000000000000000, -3.393184225085859929 ) ) ;
#49946=ORIENTED_EDGE ( 'NONE', *, *, #55813, .T. ) ;
#50114=ORIENTED_EDGE ( 'NONE', *, *, #78523, .T. ) ;
#50135=CARTESIAN_POINT ( 'NONE',  ( 0.000000000000000000, 0.000000000000000000, -1.971869939371574620 ) ) ;
#50166=CARTESIAN_POINT ( 'NONE',  ( 0.000000000000000000, 0.000000000000000000, 1.734723475976807094E-15 ) ) ;
#50334=CARTESIAN_POINT ( 'NONE',  ( 0.000000000000000000, 0.000000000000000000, -0.5505556536572887572 ) ) ;
#50503=CARTESIAN_POINT ( 'NONE',  ( 4.999999999999999112, 5.773502691896258199, -7.063244554130000630 ) ) ;
#50535=CARTESIAN_POINT ( 'NONE',  ( -5.335963852939137553, -6.035591050534815594, -7.593821156097424918 ) ) ;
#50584=CIRCLE ( 'NONE', #91959, 4.250000000000000000 ) ;
#50620=CARTESIAN_POINT ( 'NONE',  ( 0.000000000000000000, 0.000000000000000000, -10.00000000000000000 ) ) ;
#50682=B_SPLINE_CURVE_WITH_KNOTS ( 'NONE', 3,
 ( #17827, #26476, #99788, #76039, #33481, #2136, #83595, #9701, #98707, #8113 ),
 .UNSPECIFIED., .F., .F.,
 ( 4, 2, 2, 2, 4 ),
 ( 0.000000000000000000, 0.002305503304226491201, 0.004611006608452982401, 0.006916509912679473168, 0.009222013216905966537 ),
 .UNSPECIFIED. ) ;
#50811=DIRECTION ( 'NONE',  ( 1.000000000000000000, 0.000000000000000000, 0.000000000000000000 ) ) ;
#50818=CARTESIAN_POINT ( 'NONE',  ( -7.703920929261755646, -4.447860822324870789, -7.917989418073283048 ) ) ;
#50835=DIRECTION ( 'NONE',  ( 1.000000000000000000, 0.000000000000000000, 0.000000000000000000 ) ) ;
#50836=CARTESIAN_POINT ( 'NONE',  ( 7.500000000000000000, 4.330127018922203419, -0.9999999999999974465 ) ) ;
#50890=EDGE_LOOP ( 'NONE', ( #2509, #35645, #42955, #47243, #3700 ) ) ;
#50910=ORIENTED_EDGE ( 'NONE', *, *, #19561, .T. ) ;
#50936=DIRECTION ( 'NONE',  ( -0.000000000000000000, -0.000000000000000000, 1.000000000000000000 ) ) ;
#50974=VECTOR ( 'NONE', #84858, 1000.000000000000000 ) ;
#51024=AXIS2_PLACEMENT_3D ( 'NONE', #97885, #6753, #80106 ) ;
#51035=EDGE_CURVE ( 'NONE', #14360, #24961, #78603, .T. ) ;
#51037=CARTESIAN_POINT ( 'NONE',  ( -2.352990130084491319E-16, 8.660254037844390851, -7.422398894150036064 ) ) ;
#51067=FACE_OUTER_BOUND ( 'NONE', #35194, .T. ) ;
#51068=CARTESIAN_POINT ( 'NONE',  ( -2.621328321947687723, -7.606199919103087126, -7.633618187056816495 ) ) ;
#51088=CARTESIAN_POINT ( 'NONE',  ( 0.000000000000000000, 0.000000000000000000, 1.734723475976807094E-15 ) ) ;
#51135=DIRECTION ( 'NONE',  ( 0.000000000000000000, 0.000000000000000000, 1.000000000000000000 ) ) ;
#51240=CARTESIAN_POINT ( 'NONE',  ( 3.288228914120473245, -7.217643567644816294, -7.591235721156639471 ) ) ;
#51250=AXIS2_PLACEMENT_3D ( 'NONE', #23071, #47312, #81265 ) ;
#51323=AXIS2_PLACEMENT_3D ( 'NONE', #18280, #51135, #77560 ) ;
#51371=CARTESIAN_POINT ( 'NONE',  ( -1.843253007570911225E-16, -9.147862274876562338, -8.047472243342939535 ) ) ;
#51435=CIRCLE ( 'NONE', #85968, 10.12668159690567649 ) ;
#51497=CARTESIAN_POINT ( 'NONE',  ( 7.500000000000000000, -4.330127018922200755, -7.422398894150036064 ) ) ;
#51607=EDGE_LOOP ( 'NONE', ( #95369, #36851, #31672, #25221 ) ) ;
#51616=DIRECTION ( 'NONE',  ( -0.000000000000000000, -0.000000000000000000, -1.000000000000000000 ) ) ;
#51631=CARTESIAN_POINT ( 'NONE',  ( -2.325424218462540882, 7.317669739334965229, -7.030005583190789054 ) ) ;
#51673=CYLINDRICAL_SURFACE ( 'NONE', #10070, 4.250000000000000000 ) ;
#51745=CARTESIAN_POINT ( 'NONE',  ( 0.000000000000000000, 0.000000000000000000, -10.00000000000000000 ) ) ;
#51783=CARTESIAN_POINT ( 'NONE',  ( 7.922281120364393914, -4.573931137438281169, -8.047472243342934206 ) ) ;
#51821=AXIS2_PLACEMENT_3D ( 'NONE', #88615, #6623, #79977 ) ;
#51850=CARTESIAN_POINT ( 'NONE',  ( 7.499999999999999112, -1.443375672974070989, -7.063244554130000630 ) ) ;
#51901=ORIENTED_EDGE ( 'NONE', *, *, #41286, .F. ) ;
#51952=CARTESIAN_POINT ( 'NONE',  ( 7.500000000000001776, -4.330127018922199866, -0.9999999999999974465 ) ) ;
#51983=ORIENTED_EDGE ( 'NONE', *, *, #28654, .F. ) ;
#52217=ORIENTED_EDGE ( 'NONE', *, *, #97157, .F. ) ;
#52225=CARTESIAN_POINT ( 'NONE',  ( 8.472476921446266750E-16, 8.716839668575683930, -7.700121441565846325 ) ) ;
#52259=EDGE_LOOP ( 'NONE', ( #8165, #71817, #37103, #27733, #104591 ) ) ;
#52298=MECHANICAL_DESIGN_GEOMETRIC_PRESENTATION_REPRESENTATION('',(#47140),#608);
#52379=CARTESIAN_POINT ( 'NONE',  ( 7.500000000000000000, 4.330127018922189208, -7.422398894150033399 ) ) ;
#52400=CARTESIAN_POINT ( 'NONE',  ( 1.734723475976807094E-15, 8.660254037844390851, 0.000000000000000000 ) ) ;
#52551=CARTESIAN_POINT ( 'NONE',  ( 0.000000000000000000, 0.000000000000000000, -8.028130060628445364 ) ) ;
#52934=CARTESIAN_POINT ( 'NONE',  ( 5.040301471719072168, 5.750234626350511746, -0.09933465333850823031 ) ) ;
#52946=VERTEX_POINT ( 'NONE', #94133 ) ;
#53001=CARTESIAN_POINT ( 'NONE',  ( 0.000000000000000000, 0.000000000000000000, -7.657127082228716297 ) ) ;
#53022=FACE_OUTER_BOUND ( 'NONE', #4461, .T. ) ;
#53023=VERTEX_POINT ( 'NONE', #105408 ) ;
#53110=B_SPLINE_CURVE_WITH_KNOTS ( 'NONE', 3,
 ( #61703, #68722, #27760, #102664, #69772, #2358, #36384, #93521, #86512 ),
 .UNSPECIFIED., .F., .F.,
 ( 4, 2, 1, 2, 4 ),
 ( 0.000000000000000000, 0.002165063509461097498, 0.004330127018922194995, 0.006495190528383292493, 0.008660254037844389990 ),
 .UNSPECIFIED. ) ;
#53163=CARTESIAN_POINT ( 'NONE',  ( -7.500000000000000888, 0.000000000000000000, 1.734723475976807094E-15 ) ) ;
#53323=ORIENTED_EDGE ( 'NONE', *, *, #6584, .T. ) ;
#53366=EDGE_CURVE ( 'NONE', #44884, #90212, #90003, .T. ) ;
#53408=EDGE_LOOP ( 'NONE', ( #54871, #4981, #66795, #38185 ) ) ;
#53412=ORIENTED_EDGE ( 'NONE', *, *, #89996, .F. ) ;
#53483=PLANE ( 'NONE',  #66097 ) ;
#53526=CONICAL_SURFACE ( 'NONE', #75860, 4.250000000000000000, 0.9599310885968754814 ) ;
#53559=FACE_OUTER_BOUND ( 'NONE', #32108, .T. ) ;
#53634=EDGE_LOOP ( 'NONE', ( #96726, #21448 ) ) ;
#53766=AXIS2_PLACEMENT_3D ( 'NONE', #22496, #73096, #30575 ) ;
#53843=CARTESIAN_POINT ( 'NONE',  ( 3.750000000000007105, 6.495190528383288253, 1.734723475976807094E-15 ) ) ;
#53852=FACE_OUTER_BOUND ( 'NONE', #85347, .T. ) ;
#53898=EDGE_CURVE ( 'NONE', #53023, #72526, #36093, .T. ) ;
#53921=CARTESIAN_POINT ( 'NONE',  ( -4.250000000000000000, 5.204748896376250699E-16, -6.606815774914157835 ) ) ;
#54053=ORIENTED_EDGE ( 'NONE', *, *, #77588, .T. ) ;
#54069=B_SPLINE_CURVE_WITH_KNOTS ( 'NONE', 3,
 ( #2028, #65179, #98072, #89986, #16093, #48972 ),
 .UNSPECIFIED., .F., .F.,
 ( 4, 2, 4 ),
 ( 0.000000000000000000, 0.0004189869898914155171, 0.0008379739797828289743 ),
 .UNSPECIFIED. ) ;
#54170=CARTESIAN_POINT ( 'NONE',  ( -1.206569728928480911, -7.963640680051490506, -0.4524126574264524248 ) ) ;
#54204=ORIENTED_EDGE ( 'NONE', *, *, #101977, .F. ) ;
#54209=DIRECTION ( 'NONE',  ( 0.000000000000000000, 0.000000000000000000, 1.000000000000000000 ) ) ;
#54476=FACE_OUTER_BOUND ( 'NONE', #20209, .T. ) ;
#54490=EDGE_CURVE ( 'NONE', #35664, #55329, #3233, .T. ) ;
#54632=DIRECTION ( 'NONE',  ( -0.000000000000000000, -0.000000000000000000, -1.000000000000000000 ) ) ;
#54738=ADVANCED_FACE ( 'NONE', ( #5227 ), #72071, .T. ) ;
#54790=VECTOR ( 'NONE', #30729, 1000.000000000000000 ) ;
#54871=ORIENTED_EDGE ( 'NONE', *, *, #89579, .F. ) ;
#54887=CARTESIAN_POINT ( 'NONE',  ( -7.500000000000000000, 4.330127018922188320, -10.00000000000000000 ) ) ;
#54912=CONICAL_SURFACE ( 'NONE', #36034, 4.250000000000000000, 0.9599310885968754814 ) ;
#54928=CARTESIAN_POINT ( 'NONE',  ( 0.000000000000000000, 0.000000000000000000, -4.289342857142857568 ) ) ;
#54953=AXIS2_PLACEMENT_3D ( 'NONE', #51088, #66221, #18784 ) ;
#54954=VERTEX_POINT ( 'NONE', #104304 ) ;
#54970=FACE_OUTER_BOUND ( 'NONE', #37398, .T. ) ;
#54978=CARTESIAN_POINT ( 'NONE',  ( 0.000000000000000000, 0.000000000000000000, 0.000000000000000000 ) ) ;
#55074=CARTESIAN_POINT ( 'NONE',  ( -4.250000000000000000, 5.204748896376250699E-16, -10.00000000000000000 ) ) ;
#55329=VERTEX_POINT ( 'NONE', #76581 ) ;
#55366=EDGE_LOOP ( 'NONE', ( #439, #13625, #70865, #10148 ) ) ;
#55522=AXIS2_PLACEMENT_3D ( 'NONE', #85474, #84407, #34287 ) ;
#55584=CARTESIAN_POINT ( 'NONE',  ( 0.000000000000000000, 0.000000000000000000, -5.710657142857142432 ) ) ;
#55769=EDGE_CURVE ( 'NONE', #22401, #71702, #97235, .T. ) ;
#55800=CARTESIAN_POINT ( 'NONE',  ( 0.000000000000000000, 0.000000000000000000, -5.185501489199872083 ) ) ;
#55813=EDGE_CURVE ( 'NONE', #81667, #76808, #33588, .T. ) ;
#55852=CARTESIAN_POINT ( 'NONE',  ( 7.500000000000000000, 4.330127018922189208, -10.00000000000000000 ) ) ;
#55879=ORIENTED_EDGE ( 'NONE', *, *, #85442, .T. ) ;
#55933=ORIENTED_EDGE ( 'NONE', *, *, #32633, .F. ) ;
#55936=DIRECTION ( 'NONE',  ( 0.000000000000000000, 0.000000000000000000, 1.000000000000000000 ) ) ;
#55953=FACE_OUTER_BOUND ( 'NONE', #55366, .T. ) ;
#55999=ADVANCED_FACE ( 'NONE', ( #77276 ), #21519, .F. ) ;
#56141=EDGE_CURVE ( 'NONE', #13350, #49340, #82028, .T. ) ;
#56219=ORIENTED_EDGE ( 'NONE', *, *, #56141, .T. ) ;
#56221=ADVANCED_FACE ( 'NONE', ( #74470 ), #33662, .T. ) ;
#56229=EDGE_CURVE ( 'NONE', #53023, #93010, #35373, .T. ) ;
#56286=EDGE_CURVE ( 'NONE', #87281, #75707, #16333, .T. ) ;
#56337=CARTESIAN_POINT ( 'NONE',  ( 7.500000000000000888, 0.000000000000000000, 1.734723475976807094E-15 ) ) ;
#56389=CIRCLE ( 'NONE', #25513, 5.000000000000000000 ) ;
#56440=B_SPLINE_CURVE_WITH_KNOTS ( 'NONE', 3,
 ( #46116, #104877, #54170, #5121, #38565, #103804 ),
 .UNSPECIFIED., .F., .F.,
 ( 4, 2, 4 ),
 ( 2.475503369437265404E-07, 0.002222330217055646685, 0.004444412883774349725 ),
 .UNSPECIFIED. ) ;
#56460=AXIS2_PLACEMENT_3D ( 'NONE', #54978, #31800, #46896 ) ;
#56464=EDGE_LOOP ( 'NONE', ( #58450, #28147, #30208, #46993 ) ) ;
#56510=ORIENTED_EDGE ( 'NONE', *, *, #100290, .F. ) ;
#56549=PLANE ( 'NONE',  #101150 ) ;
#56561=ORIENTED_EDGE ( 'NONE', *, *, #40757, .F. ) ;
#56620=AXIS2_PLACEMENT_3D ( 'NONE', #87082, #47124, #14749 ) ;
#56626=ADVANCED_FACE ( 'NONE', ( #75952 ), #18825, .F. ) ;
#56667=DIRECTION ( 'NONE',  ( -0.000000000000000000, -0.000000000000000000, 1.000000000000000000 ) ) ;
#56670=VECTOR ( 'NONE', #24589, 1000.000000000000000 ) ;
#56697=CARTESIAN_POINT ( 'NONE',  ( 4.250000000000000000, 0.000000000000000000, -10.00000000000000000 ) ) ;
#56809=ADVANCED_FACE ( 'NONE', ( #94818 ), #94004, .T. ) ;
#56851=CARTESIAN_POINT ( 'NONE',  ( 5.112021521199307195, -5.708827036476817440, -7.069802615102037890 ) ) ;
#56868=DIRECTION ( 'NONE',  ( -0.000000000000000000, -0.000000000000000000, 1.000000000000000000 ) ) ;
#56870=ORIENTED_EDGE ( 'NONE', *, *, #3671, .F. ) ;
#56889=ORIENTED_EDGE ( 'NONE', *, *, #2572, .T. ) ;
#57033=DIRECTION ( 'NONE',  ( 0.000000000000000000, 0.000000000000000000, 1.000000000000000000 ) ) ;
#57060=CARTESIAN_POINT ( 'NONE',  ( -7.500000000000000000, 4.330127018922188320, -7.422398894150033399 ) ) ;
#57083=CIRCLE ( 'NONE', #39863, 4.250000000000000000 ) ;
#57089=DIRECTION ( 'NONE',  ( -1.000000000000000000, 0.000000000000000000, 0.000000000000000000 ) ) ;
#57109=ADVANCED_FACE ( 'NONE', ( #53022 ), #9675, .F. ) ;
#57131=FACE_OUTER_BOUND ( 'NONE', #79464, .T. ) ;
#57170=EDGE_CURVE ( 'NONE', #34186, #29730, #14851, .T. ) ;
#57242=CARTESIAN_POINT ( 'NONE',  ( -7.914984360234579519, 3.818534719232086871, -7.907701344400643428 ) ) ;
#57292=VERTEX_POINT ( 'NONE', #64306 ) ;
#57296=CARTESIAN_POINT ( 'NONE',  ( 0.000000000000000000, 0.000000000000000000, -7.657127082228716297 ) ) ;
#57379=CARTESIAN_POINT ( 'NONE',  ( 1.015826369459132961, -8.073766409984528991, -7.642786413616108554 ) ) ;
#57431=( NAMED_UNIT ( * ) SI_UNIT ( $, .STERADIAN. ) SOLID_ANGLE_UNIT ( ) );
#57517=ORIENTED_EDGE ( 'NONE', *, *, #89354, .F. ) ;
#57524=EDGE_LOOP ( 'NONE', ( #100474, #101325, #60966, #44767, #10184 ) ) ;
#57536=EDGE_LOOP ( 'NONE', ( #67867, #13261, #86012, #96785 ) ) ;
#57562=LINE ( 'NONE', #24194, #96066 ) ;
#57596=AXIS2_PLACEMENT_3D ( 'NONE', #2251, #59467, #68072 ) ;
#57622=AXIS2_PLACEMENT_3D ( 'NONE', #4897, #4357, #105175 ) ;
#57698=DIRECTION ( 'NONE',  ( 0.000000000000000000, 0.000000000000000000, 1.000000000000000000 ) ) ;
#57714=VECTOR ( 'NONE', #25447, 1000.000000000000000 ) ;
#57721=CARTESIAN_POINT ( 'NONE',  ( 7.922811941611899833, 4.628808333142398368, -8.057670691780701944 ) ) ;
#57728=VERTEX_POINT ( 'NONE', #17167 ) ;
#57910=CARTESIAN_POINT ( 'NONE',  ( -0.2779000157839468521, -8.820699686765063774, -7.928862157988307402 ) ) ;
#57914=CARTESIAN_POINT ( 'NONE',  ( -7.908219015560238319, -3.084967917785943037, -7.795665562178440311 ) ) ;
#57975=DIRECTION ( 'NONE',  ( 0.8191520442889884679, 0.000000000000000000, 0.5735764363510508224 ) ) ;
#58004=FACE_OUTER_BOUND ( 'NONE', #7086, .T. ) ;
#58152=EDGE_CURVE ( 'NONE', #32589, #76808, #10641, .T. ) ;
#58286=CARTESIAN_POINT ( 'NONE',  ( 0.000000000000000000, 0.000000000000000000, -6.606815774914157835 ) ) ;
#58299=DIRECTION ( 'NONE',  ( -0.000000000000000000, -0.000000000000000000, 1.000000000000000000 ) ) ;
#58342=ORIENTED_EDGE ( 'NONE', *, *, #2580, .F. ) ;
#58450=ORIENTED_EDGE ( 'NONE', *, *, #17543, .F. ) ;
#58464=DIRECTION ( 'NONE',  ( 0.8660254037844382635, -0.5000000000000005551, 0.000000000000000000 ) ) ;
#58484=CARTESIAN_POINT ( 'NONE',  ( 2.621086668468698200, 7.606368536631365806, -7.634085501268429219 ) ) ;
#58546=CARTESIAN_POINT ( 'NONE',  ( 2.503857664561936320E-16, -8.660254037844401509, -7.422398894150040505 ) ) ;
#58578=AXIS2_PLACEMENT_3D ( 'NONE', #74692, #774, #99501 ) ;
#58593=ORIENTED_EDGE ( 'NONE', *, *, #100844, .F. ) ;
#58628=CARTESIAN_POINT ( 'NONE',  ( 7.500000000000000000, 4.330127018922189208, -7.422398894150033399 ) ) ;
#58679=CARTESIAN_POINT ( 'NONE',  ( -2.352174619740411643, 7.302225387955492586, -7.450218641348505422 ) ) ;
#58687=DIRECTION ( 'NONE',  ( -0.000000000000000000, -0.000000000000000000, 1.000000000000000000 ) ) ;
#58848=ORIENTED_EDGE ( 'NONE', *, *, #78866, .T. ) ;
#58909=ORIENTED_EDGE ( 'NONE', *, *, #18809, .T. ) ;
#58940=CARTESIAN_POINT ( 'NONE',  ( -6.874999999999997335, 4.690970937165706900, -7.298562697733107285 ) ) ;
#59005=CARTESIAN_POINT ( 'NONE',  ( 6.901579824520447382, -4.675625068323824962, -0.7022220667781352565 ) ) ;
#59018=CARTESIAN_POINT ( 'NONE',  ( 4.606548227981510202, 6.456511556909250160, -7.591235721156635030 ) ) ;
#59052=VERTEX_POINT ( 'NONE', #50836 ) ;
#59065=CARTESIAN_POINT ( 'NONE',  ( 5.000000000000000000, 6.123233995736766282E-16, -5.710657142857142432 ) ) ;
#59121=CARTESIAN_POINT ( 'NONE',  ( -7.500000000000000000, 4.330127018922188320, -0.9999999999999904521 ) ) ;
#59192=ORIENTED_EDGE ( 'NONE', *, *, #84078, .T. ) ;
#59327=CARTESIAN_POINT ( 'NONE',  ( -7.500000000000000000, -4.330127018922203419, -0.9999999999999974465 ) ) ;
#59345=CARTESIAN_POINT ( 'NONE',  ( 4.250000000000000000, 0.000000000000000000, -4.814498510800145681 ) ) ;
#59467=DIRECTION ( 'NONE',  ( 0.000000000000000000, 0.000000000000000000, 1.000000000000000000 ) ) ;
#59521=AXIS2_PLACEMENT_3D ( 'NONE', #6951, #15040, #57089 ) ;
#59531=AXIS2_PLACEMENT_3D ( 'NONE', #38430, #103146, #104723 ) ;
#59547=ORIENTED_EDGE ( 'NONE', *, *, #85871, .F. ) ;
#59576=DIRECTION ( 'NONE',  ( -1.000000000000000000, 0.000000000000000000, 0.000000000000000000 ) ) ;
#59595=VECTOR ( 'NONE', #81297, 1000.000000000000000 ) ;
#59673=UNCERTAINTY_MEASURE_WITH_UNIT (LENGTH_MEASURE( 1.000000000000000082E-05 ), #87462, 'distance_accuracy_value', 'NONE');
#59678=CIRCLE ( 'NONE', #28675, 4.250000000000000000 ) ;
#59730=CARTESIAN_POINT ( 'NONE',  ( -5.147825380260277583, -5.688155668810499499, -7.450218641349906079 ) ) ;
#59749=FACE_OUTER_BOUND ( 'NONE', #13660, .T. ) ;
#59788=ORIENTED_EDGE ( 'NONE', *, *, #65240, .T. ) ;
#59810=ORIENTED_EDGE ( 'NONE', *, *, #3730, .F. ) ;
#59873=AXIS2_PLACEMENT_3D ( 'NONE', #66463, #10727, #45257 ) ;
#59964=EDGE_CURVE ( 'NONE', #95526, #26814, #27130, .T. ) ;
#60124=CARTESIAN_POINT ( 'NONE',  ( 7.922281120364393914, 4.573931137438267847, -8.047472243342932430 ) ) ;
#60215=FACE_OUTER_BOUND ( 'NONE', #22112, .T. ) ;
#60305=VERTEX_POINT ( 'NONE', #27044 ) ;
#60417=DIRECTION ( 'NONE',  ( 0.000000000000000000, 0.000000000000000000, -1.000000000000000000 ) ) ;
#60461=CARTESIAN_POINT ( 'NONE',  ( -4.633158437802761763E-12, -9.016621985895911351, -7.999704684617491068 ) ) ;
#60478=ORIENTED_EDGE ( 'NONE', *, *, #54490, .T. ) ;
#60525=PRODUCT_DEFINITION_SHAPE ( 'NONE', 'NONE',  #98978 ) ;
#60550=CARTESIAN_POINT ( 'NONE',  ( -7.549004593702462351, -4.358419834287845518, -7.700121441565844549 ) ) ;
#60565=EDGE_CURVE ( 'NONE', #57292, #55329, #56389, .T. ) ;
#60635=ORIENTED_EDGE ( 'NONE', *, *, #100844, .T. ) ;
#60829=ADVANCED_FACE ( 'NONE', ( #82456 ), #65119, .F. ) ;
#60848=ORIENTED_EDGE ( 'NONE', *, *, #85871, .T. ) ;
#60957=ORIENTED_EDGE ( 'NONE', *, *, #83379, .F. ) ;
#60966=ORIENTED_EDGE ( 'NONE', *, *, #6280, .F. ) ;
#61045=CARTESIAN_POINT ( 'NONE',  ( 4.403473400622099021, 6.117907484625860093, 2.340352033263631048E-15 ) ) ;
#61050=ORIENTED_EDGE ( 'NONE', *, *, #92666, .T. ) ;
#61235=CARTESIAN_POINT ( 'NONE',  ( 0.000000000000000000, 0.000000000000000000, -2.868028571428571372 ) ) ;
#61324=ORIENTED_EDGE ( 'NONE', *, *, #25006, .T. ) ;
#61392=CONICAL_SURFACE ( 'NONE', #97532, 5.000000000000000000, 0.9599310885968913576 ) ;
#61429=EDGE_CURVE ( 'NONE', #83574, #38530, #78759, .T. ) ;
#61457=DIRECTION ( 'NONE',  ( 1.000000000000000000, 0.000000000000000000, 0.000000000000000000 ) ) ;
#61536=ORIENTED_EDGE ( 'NONE', *, *, #36390, .T. ) ;
#61614=VECTOR ( 'NONE', #103104, 1000.000000000000000 ) ;
#61623=CARTESIAN_POINT ( 'NONE',  ( 7.500000000000000000, 1.572594658376116339, -7.069792055233641292 ) ) ;
#61703=CARTESIAN_POINT ( 'NONE',  ( -7.500000000000000000, 4.330127018922188320, -7.422398894150033399 ) ) ;
#61764=AXIS2_PLACEMENT_3D ( 'NONE', #50135, #3188, #43642 ) ;
#61780=DIRECTION ( 'NONE',  ( -1.000000000000000000, 0.000000000000000000, 0.000000000000000000 ) ) ;
#61794=ORIENTED_EDGE ( 'NONE', *, *, #74327, .F. ) ;
#61886=CARTESIAN_POINT ( 'NONE',  ( -5.000000000000000888, 6.123233995736767268E-16, -25.03750572909317285 ) ) ;
#61959=AXIS2_PLACEMENT_3D ( 'NONE', #101372, #18348, #85183 ) ;
#61983=CARTESIAN_POINT ( 'NONE',  ( 5.000000000000000000, 6.123233995736766282E-16, -0.02540000000000007530 ) ) ;
#62026=CONICAL_SURFACE ( 'NONE', #48199, 7.500000000000000888, 0.8594454914424817238 ) ;
#62049=CIRCLE ( 'NONE', #36196, 5.000000000000000000 ) ;
#62106=EDGE_CURVE ( 'NONE', #18346, #24961, #19530, .T. ) ;
#62138=CARTESIAN_POINT ( 'NONE',  ( -4.250000000000000000, 5.204748896376250699E-16, -7.657127082228716297 ) ) ;
#62146=AXIS2_PLACEMENT_3D ( 'NONE', #30666, #55936, #31204 ) ;
#62153=CARTESIAN_POINT ( 'NONE',  ( 7.922798488042200660, -4.627419312545549168, -8.057411459260043429 ) ) ;
#62254=VERTEX_POINT ( 'NONE', #68582 ) ;
#62302=EDGE_CURVE ( 'NONE', #49340, #81388, #784, .T. ) ;
#62371=ORIENTED_EDGE ( 'NONE', *, *, #47973, .F. ) ;
#62384=DIRECTION ( 'NONE',  ( -0.8191520442889884679, 1.003171929053520679E-16, 0.5735764363510508224 ) ) ;
#62476=ORIENTED_EDGE ( 'NONE', *, *, #93433, .T. ) ;
#62488=CARTESIAN_POINT ( 'NONE',  ( 2.503857664561936320E-16, -8.660254037844401509, -10.00000000000000000 ) ) ;
#62544=CARTESIAN_POINT ( 'NONE',  ( 0.3306966981844232656, 8.469326210127494647, -7.349897473154332062 ) ) ;
#62575=CIRCLE ( 'NONE', #76331, 5.000000000000000000 ) ;
#62587=EDGE_CURVE ( 'NONE', #34113, #73538, #80227, .T. ) ;
#62589=ORIENTED_EDGE ( 'NONE', *, *, #84381, .T. ) ;
#62658=PRESENTATION_STYLE_ASSIGNMENT (( #70732 ) ) ;
#62669=DIRECTION ( 'NONE',  ( 0.000000000000000000, 0.000000000000000000, 1.000000000000000000 ) ) ;
#62673=CARTESIAN_POINT ( 'NONE',  ( 0.000000000000000000, 0.000000000000000000, -9.974599999999998801 ) ) ;
#62676=DIRECTION ( 'NONE',  ( -1.000000000000000000, 0.000000000000000000, 0.000000000000000000 ) ) ;
#62723=DIRECTION ( 'NONE',  ( -0.000000000000000000, -0.000000000000000000, -1.000000000000000000 ) ) ;
#62811=DIRECTION ( 'NONE',  ( -1.000000000000000000, 0.000000000000000000, 0.000000000000000000 ) ) ;
#62962=VERTEX_POINT ( 'NONE', #84 ) ;
#62963=VECTOR ( 'NONE', #62669, 1000.000000000000000 ) ;
#63023=CARTESIAN_POINT ( 'NONE',  ( 0.000000000000000000, 0.000000000000000000, -6.235812796514431433 ) ) ;
#63073=CARTESIAN_POINT ( 'NONE',  ( 7.777900015783949961, 4.169681370001524279, -7.928862157988302073 ) ) ;
#63187=ADVANCED_FACE ( 'NONE', ( #10851 ), #28692, .F. ) ;
#63204=DIRECTION ( 'NONE',  ( 0.000000000000000000, 0.000000000000000000, 1.000000000000000000 ) ) ;
#63259=LINE ( 'NONE', #96150, #47259 ) ;
#63388=ORIENTED_EDGE ( 'NONE', *, *, #70530, .F. ) ;
#63422=CARTESIAN_POINT ( 'NONE',  ( 7.500000000000002665, -0.7512838658081426590, 2.480112469560591787E-15 ) ) ;
#63547=DIRECTION ( 'NONE',  ( -0.000000000000000000, -0.000000000000000000, -1.000000000000000000 ) ) ;
#63564=DIRECTION ( 'NONE',  ( 1.000000000000000000, 0.000000000000000000, 0.000000000000000000 ) ) ;
#63592=EDGE_CURVE ( 'NONE', #29730, #62962, #17661, .T. ) ;
#63618=CONICAL_SURFACE ( 'NONE', #54953, 7.500000000000000888, 0.8594454914424817238 ) ;
#63741=CARTESIAN_POINT ( 'NONE',  ( 0.000000000000000000, 0.000000000000000000, -10.00000000000000000 ) ) ;
#63816=CARTESIAN_POINT ( 'NONE',  ( 0.000000000000000000, 0.000000000000000000, -10.00000000000000000 ) ) ;
#63858=DIRECTION ( 'NONE',  ( 0.8191520442889884679, 0.000000000000000000, 0.5735764363510508224 ) ) ;
#63879=PLANE ( 'NONE',  #12244 ) ;
#63890=ADVANCED_FACE ( 'NONE', ( #86136 ), #70983, .F. ) ;
#63941=CARTESIAN_POINT ( 'NONE',  ( -7.500000000000000888, 0.000000000000000000, 1.734723475976807094E-15 ) ) ;
#63985=AXIS2_PLACEMENT_3D ( 'NONE', #98427, #16996, #49331 ) ;
#64087=VERTEX_POINT ( 'NONE', #97503 ) ;
#64096=DIRECTION ( 'NONE',  ( -1.000000000000000000, 0.000000000000000000, 0.000000000000000000 ) ) ;
#64132=CARTESIAN_POINT ( 'NONE',  ( -1.211595439868049962, 7.960739084487649109, -0.4504974108211952655 ) ) ;
#64213=CARTESIAN_POINT ( 'NONE',  ( 0.000000000000000000, 0.000000000000000000, 1.734723475976807094E-15 ) ) ;
#64263=VECTOR ( 'NONE', #106136, 1000.000000000000000 ) ;
#64306=CARTESIAN_POINT ( 'NONE',  ( -5.000000000000000000, 0.000000000000000000, -7.131971428571428184 ) ) ;
#64379=ORIENTED_EDGE ( 'NONE', *, *, #18234, .F. ) ;
#64403=CARTESIAN_POINT ( 'NONE',  ( 1.734723475976807094E-15, 8.660254037844390851, -10.00000000000000000 ) ) ;
#64446=ADVANCED_FACE ( 'NONE', ( #98451 ), #44185, .F. ) ;
#64670=CARTESIAN_POINT ( 'NONE',  ( -5.000000000000000000, 0.000000000000000000, -4.289342857142857568 ) ) ;
#64675=CONICAL_SURFACE ( 'NONE', #78458, 4.250000000000000000, 0.9599310885968754814 ) ;
#64862=CARTESIAN_POINT ( 'NONE',  ( 7.922281120364393914, 4.573931137438267847, -8.047472243342932430 ) ) ;
#65119=CONICAL_SURFACE ( 'NONE', #46192, 4.250000000000000000, 0.9599310885968754814 ) ;
#65179=CARTESIAN_POINT ( 'NONE',  ( 7.500000000000007105, -4.330127018922198090, -7.564338275809343592 ) ) ;
#65192=VERTEX_POINT ( 'NONE', #19053 ) ;
#65204=ORIENTED_EDGE ( 'NONE', *, *, #26591, .F. ) ;
#65208=CIRCLE ( 'NONE', #36013, 5.000000000000000000 ) ;
#65240=EDGE_CURVE ( 'NONE', #72931, #20962, #72842, .T. ) ;
#65318=ORIENTED_EDGE ( 'NONE', *, *, #92045, .T. ) ;
#65327=DIRECTION ( 'NONE',  ( -1.000000000000000000, 0.000000000000000000, 0.000000000000000000 ) ) ;
#65397=ORIENTED_EDGE ( 'NONE', *, *, #40958, .T. ) ;
#65465=ORIENTED_EDGE ( 'NONE', *, *, #62587, .F. ) ;
#65478=TOROIDAL_SURFACE ( 'NONE', #24233, 10.12668159690567826, 0.7733184030943209830 ) ;
#65485=EDGE_LOOP ( 'NONE', ( #46506, #99712, #54204, #65204 ) ) ;
#65604=CARTESIAN_POINT ( 'NONE',  ( -2.621086668468698200, -7.606368536631376465, -7.634085501268432772 ) ) ;
#65637=CARTESIAN_POINT ( 'NONE',  ( 0.000000000000000000, 0.000000000000000000, 1.734723475976807094E-15 ) ) ;
#65702=FACE_OUTER_BOUND ( 'NONE', #77995, .T. ) ;
#65736=EDGE_LOOP ( 'NONE', ( #92788, #38191, #5157, #62371, #72320, #100897 ) ) ;
#65865=LINE ( 'NONE', #98745, #5909 ) ;
#65955=CARTESIAN_POINT ( 'NONE',  ( 0.000000000000000000, 0.000000000000000000, -5.710657142857142432 ) ) ;
#65981=ORIENTED_EDGE ( 'NONE', *, *, #54490, .F. ) ;
#65985=CIRCLE ( 'NONE', #10847, 4.250000000000000000 ) ;
#66037=DIRECTION ( 'NONE',  ( 0.000000000000000000, 0.000000000000000000, 1.000000000000000000 ) ) ;
#66047=ORIENTED_EDGE ( 'NONE', *, *, #18234, .T. ) ;
#66086=COLOUR_RGB ( '', 0.08235294, 0.09019608, 0.10196078) ;
#66097=AXIS2_PLACEMENT_3D ( 'NONE', #52400, #21157, #11405 ) ;
#66109=ORIENTED_EDGE ( 'NONE', *, *, #20690, .T. ) ;
#66132=CARTESIAN_POINT ( 'NONE',  ( -7.263825692932297962, -4.945657111639586212, -7.907570769506051533 ) ) ;
#66221=DIRECTION ( 'NONE',  ( 0.000000000000000000, 0.000000000000000000, -1.000000000000000000 ) ) ;
#66335=ORIENTED_EDGE ( 'NONE', *, *, #17744, .F. ) ;
#66389=CARTESIAN_POINT ( 'NONE',  ( 4.250000000000000000, 0.000000000000000000, -0.5505556536572887572 ) ) ;
#66444=DIRECTION ( 'NONE',  ( -0.8191520442889884679, 1.003171929053520679E-16, 0.5735764363510508224 ) ) ;
#66463=CARTESIAN_POINT ( 'NONE',  ( 0.000000000000000000, 0.000000000000000000, -8.500000000000000000 ) ) ;
#66469=ORIENTED_EDGE ( 'NONE', *, *, #105785, .F. ) ;
#66511=AXIS2_PLACEMENT_3D ( 'NONE', #18450, #91271, #42699 ) ;
#66630=VERTEX_POINT ( 'NONE', #94066 ) ;
#66699=CARTESIAN_POINT ( 'NONE',  ( -4.250000000000000000, 5.204748896376250699E-16, -9.078441367943003826 ) ) ;
#66744=CARTESIAN_POINT ( 'NONE',  ( -6.484173630543650368, -4.916614646775412822, -7.642786413614080843 ) ) ;
#66795=ORIENTED_EDGE ( 'NONE', *, *, #71487, .T. ) ;
#66883=AXIS2_PLACEMENT_3D ( 'NONE', #50166, #60417, #75500 ) ;
#66895=VECTOR ( 'NONE', #33787, 1000.000000000000000 ) ;
#66914=ORIENTED_EDGE ( 'NONE', *, *, #17517, .T. ) ;
#67058=FACE_OUTER_BOUND ( 'NONE', #18309, .T. ) ;
#67156=LINE ( 'NONE', #100041, #79561 ) ;
#67166=ORIENTED_EDGE ( 'NONE', *, *, #105785, .T. ) ;
#67174=CIRCLE ( 'NONE', #103367, 5.000000000000000000 ) ;
#67199=EDGE_CURVE ( 'NONE', #72931, #106311, #57562, .T. ) ;
#67255=CIRCLE ( 'NONE', #86200, 5.000000000000000000 ) ;
#67289=VECTOR ( 'NONE', #101913, 1000.000000000000000 ) ;
#67299=LINE ( 'NONE', #73769, #31529 ) ;
#67329=VERTEX_POINT ( 'NONE', #11142 ) ;
#67410=CARTESIAN_POINT ( 'NONE',  ( -6.874999999999999112, -4.690970937165719334, -7.298562697733108173 ) ) ;
#67446=ADVANCED_FACE ( 'NONE', ( #30555 ), #35813, .F. ) ;
#67526=DIRECTION ( 'NONE',  ( 0.5000000000000006661, -0.8660254037844382635, 0.000000000000000000 ) ) ;
#67605=DIRECTION ( 'NONE',  ( 0.000000000000000000, -1.000000000000000000, 0.000000000000000000 ) ) ;
#67621=CARTESIAN_POINT ( 'NONE',  ( 0.000000000000000000, 0.000000000000000000, -1.446714285714285841 ) ) ;
#67643=CARTESIAN_POINT ( 'NONE',  ( -6.318250223874061420E-16, 9.147862274876551680, -8.047472243342934206 ) ) ;
#67652=CARTESIAN_POINT ( 'NONE',  ( -7.922281120364393914, 4.573931137438267847, -8.047472243342932430 ) ) ;
#67668=ORIENTED_EDGE ( 'NONE', *, *, #47973, .T. ) ;
#67782=FACE_OUTER_BOUND ( 'NONE', #33931, .T. ) ;
#67791=LINE ( 'NONE', #33316, #29518 ) ;
#67810=CARTESIAN_POINT ( 'NONE',  ( -1.060314165523204677, -8.048081368954012049, -7.659344964962870428 ) ) ;
#67847=ORIENTED_EDGE ( 'NONE', *, *, #525, .T. ) ;
#67867=ORIENTED_EDGE ( 'NONE', *, *, #69048, .F. ) ;
#67919=ORIENTED_EDGE ( 'NONE', *, *, #78523, .F. ) ;
#68055=CARTESIAN_POINT ( 'NONE',  ( -4.403473400622100797, -6.117907484625871639, -6.860966872759830380E-15 ) ) ;
#68072=DIRECTION ( 'NONE',  ( 1.000000000000000000, 0.000000000000000000, 0.000000000000000000 ) ) ;
#68174=ADVANCED_FACE ( 'NONE', ( #9161 ), #84122, .T. ) ;
#68321=DIRECTION ( 'NONE',  ( 0.000000000000000000, 0.000000000000000000, 1.000000000000000000 ) ) ;
#68369=CARTESIAN_POINT ( 'NONE',  ( -6.625705691649441675, 5.306270977113046960, -7.795653906408888112 ) ) ;
#68519=EDGE_CURVE ( 'NONE', #65192, #26769, #35978, .T. ) ;
#68582=CARTESIAN_POINT ( 'NONE',  ( -4.250000000000000000, 5.204748896376250699E-16, -3.764187203485586330 ) ) ;
#68634=( NAMED_UNIT ( * ) PLANE_ANGLE_UNIT ( ) SI_UNIT ( $, .RADIAN. ) );
#68688=ORIENTED_EDGE ( 'NONE', *, *, #104253, .T. ) ;
#68722=CARTESIAN_POINT ( 'NONE',  ( -7.500000000000000000, 3.608439182435155601, -7.298562697733106397 ) ) ;
#68815=CARTESIAN_POINT ( 'NONE',  ( -4.406842699996125212, 6.115962218725286448, 2.334422802632851734E-15 ) ) ;
#68818=AXIS2_PLACEMENT_3D ( 'NONE', #39215, #71030, #13843 ) ;
#68853=UNCERTAINTY_MEASURE_WITH_UNIT (LENGTH_MEASURE( 1.000000000000000082E-05 ), #72048, 'distance_accuracy_value', 'NONE');
#68973=CARTESIAN_POINT ( 'NONE',  ( -2.352990130084491319E-16, 8.660254037844390851, -7.422398894150036064 ) ) ;
#69048=EDGE_CURVE ( 'NONE', #96921, #66630, #45949, .T. ) ;
#69150=CARTESIAN_POINT ( 'NONE',  ( 5.000000000000000000, 6.123233995736766282E-16, -2.868028571428571372 ) ) ;
#69160=CIRCLE ( 'NONE', #22660, 7.500000000000003553 ) ;
#69179=VERTEX_POINT ( 'NONE', #8121 ) ;
#69279=ADVANCED_FACE ( 'NONE', ( #47349 ), #44641, .F. ) ;
#69282=ORIENTED_EDGE ( 'NONE', *, *, #73235, .T. ) ;
#69337=ADVANCED_FACE ( 'NONE', ( #39285 ), #46471, .F. ) ;
#69356=CARTESIAN_POINT ( 'NONE',  ( -2.352990130084491319E-16, 8.660254037844390851, -10.00000000000000000 ) ) ;
#69376=DIRECTION ( 'NONE',  ( 0.8191520442889975717, 1.003171929053531773E-16, -0.5735764363510378328 ) ) ;
#69469=EDGE_CURVE ( 'NONE', #18381, #10693, #46912, .T. ) ;
#69490=EDGE_LOOP ( 'NONE', ( #17122, #97092, #70418, #6147 ) ) ;
#69528=DIRECTION ( 'NONE',  ( -1.000000000000000000, 0.000000000000000000, 0.000000000000000000 ) ) ;
#69659=CARTESIAN_POINT ( 'NONE',  ( 6.288404560131952259, 5.029641972278930062, -0.4504974108211907136 ) ) ;
#69678=( NAMED_UNIT ( * ) SI_UNIT ( $, .STERADIAN. ) SOLID_ANGLE_UNIT ( ) );
#69682=EDGE_CURVE ( 'NONE', #31711, #100365, #101522, .T. ) ;
#69690=AXIS2_PLACEMENT_3D ( 'NONE', #90402, #74198, #32174 ) ;
#69723=CARTESIAN_POINT ( 'NONE',  ( 0.000000000000000000, 0.000000000000000000, -5.185501489199872083 ) ) ;
#69772=CARTESIAN_POINT ( 'NONE',  ( -7.500000000000000000, -7.155734338404329264E-15, -6.991905250253754645 ) ) ;
#69812=CARTESIAN_POINT ( 'NONE',  ( 0.000000000000000000, 8.660254037844390851, -0.9999999999999974465 ) ) ;
#70031=DIRECTION ( 'NONE',  ( -1.000000000000000000, 0.000000000000000000, 0.000000000000000000 ) ) ;
#70033=CARTESIAN_POINT ( 'NONE',  ( 1.206569728928467589, 7.963640680051485177, -0.4524126574264484835 ) ) ;
#70133=ORIENTED_EDGE ( 'NONE', *, *, #62106, .T. ) ;
#70202=FILL_AREA_STYLE ('',( #37343 ) ) ;
#70299=DIRECTION ( 'NONE',  ( -0.000000000000000000, -0.000000000000000000, 1.000000000000000000 ) ) ;
#70342=DIRECTION ( 'NONE',  ( 0.8191520442889975717, 1.003171929053531773E-16, -0.5735764363510378328 ) ) ;
#70406=DIRECTION ( 'NONE',  ( -0.000000000000000000, -0.000000000000000000, -1.000000000000000000 ) ) ;
#70418=ORIENTED_EDGE ( 'NONE', *, *, #26591, .T. ) ;
#70430=FACE_OUTER_BOUND ( 'NONE', #79386, .T. ) ;
#70447=FACE_OUTER_BOUND ( 'NONE', #49023, .T. ) ;
#70530=EDGE_CURVE ( 'NONE', #62962, #91741, #62049, .T. ) ;
#70630=CARTESIAN_POINT ( 'NONE',  ( 5.335963852944037633, 6.035591050531996515, -7.593821156097438241 ) ) ;
#70666=ADVANCED_FACE ( 'NONE', ( #54970 ), #86222, .F. ) ;
#70715=DIRECTION ( 'NONE',  ( -1.000000000000000000, 0.000000000000000000, 0.000000000000000000 ) ) ;
#70732=SURFACE_STYLE_USAGE ( .BOTH. , #93428 ) ;
#70812=CONICAL_SURFACE ( 'NONE', #15918, 5.000000000000000000, 0.9599310885968913576 ) ;
#70826=CARTESIAN_POINT ( 'NONE',  ( 0.000000000000000000, 0.000000000000000000, -9.226681596905679683 ) ) ;
#70840=ORIENTED_EDGE ( 'NONE', *, *, #96554, .F. ) ;
#70865=ORIENTED_EDGE ( 'NONE', *, *, #89741, .T. ) ;
#70952=CARTESIAN_POINT ( 'NONE',  ( -7.500000000000000000, 4.330127018922188320, -0.9999999999999904521 ) ) ;
#70983=CYLINDRICAL_SURFACE ( 'NONE', #88909, 4.250000000000000000 ) ;
#71030=DIRECTION ( 'NONE',  ( -0.000000000000000000, 0.000000000000000000, -1.000000000000000000 ) ) ;
#71151=CARTESIAN_POINT ( 'NONE',  ( 6.484173630541964606, 4.916614646777613729, -7.642786413608825491 ) ) ;
#71181=ADVANCED_FACE ( 'NONE', ( #99426 ), #47010, .F. ) ;
#71246=AXIS2_PLACEMENT_3D ( 'NONE', #8367, #50936, #26202 ) ;
#71253=( GEOMETRIC_REPRESENTATION_CONTEXT ( 3 ) GLOBAL_UNCERTAINTY_ASSIGNED_CONTEXT ( ( #98512 ) ) GLOBAL_UNIT_ASSIGNED_CONTEXT ( ( #44885, #95030, #69678 ) ) REPRESENTATION_CONTEXT ( 'NONE', 'WORKASPACE' ) );
#71270=FACE_OUTER_BOUND ( 'NONE', #95945, .T. ) ;
#71342=FACE_OUTER_BOUND ( 'NONE', #69490, .T. ) ;
#71464=CARTESIAN_POINT ( 'NONE',  ( 5.000000000000000000, 0.000000000000000000, 0.000000000000000000 ) ) ;
#71480=ORIENTED_EDGE ( 'NONE', *, *, #30875, .F. ) ;
#71487=EDGE_CURVE ( 'NONE', #104354, #81388, #20720, .T. ) ;
#71492=B_SPLINE_CURVE_WITH_KNOTS ( 'NONE', 3,
 ( #60124, #92988, #90871, #25641, #19150, #76794 ),
 .UNSPECIFIED., .F., .F.,
 ( 4, 2, 4 ),
 ( 0.000000000000000000, 0.002307655110370370865, 0.004615310220740741730 ),
 .UNSPECIFIED. ) ;
#71506=FILL_AREA_STYLE_COLOUR ( '', #66086 ) ;
#71669=CARTESIAN_POINT ( 'NONE',  ( 0.6169862416619652512, 8.783631307151134493, -7.913704048099899246 ) ) ;
#71702=VERTEX_POINT ( 'NONE', #9763 ) ;
#71792=LINE ( 'NONE', #22228, #20881 ) ;
#71796=CYLINDRICAL_SURFACE ( 'NONE', #3111, 4.250000000000000000 ) ;
#71817=ORIENTED_EDGE ( 'NONE', *, *, #21063, .T. ) ;
#71839=ORIENTED_EDGE ( 'NONE', *, *, #36390, .F. ) ;
#71893=CIRCLE ( 'NONE', #85697, 0.7733184030943203169 ) ;
#71924=CARTESIAN_POINT ( 'NONE',  ( 7.500000000000000000, -4.330127018922200755, -10.00000000000000000 ) ) ;
#72016=DIRECTION ( 'NONE',  ( -0.8191520442889884679, 1.003171929053520679E-16, 0.5735764363510508224 ) ) ;
#72048=( LENGTH_UNIT ( ) NAMED_UNIT ( * ) SI_UNIT ( .MILLI., .METRE. ) );
#72052=VECTOR ( 'NONE', #79198, 1000.000000000000000 ) ;
#72071=PLANE ( 'NONE',  #105705 ) ;
#72101=LINE ( 'NONE', #72628, #7915 ) ;
#72156=DIRECTION ( 'NONE',  ( 1.000000000000000000, 0.000000000000000000, 0.000000000000000000 ) ) ;
#72303=CARTESIAN_POINT ( 'NONE',  ( 7.922281120364393914, -4.573931137438281169, -8.047472243342934206 ) ) ;
#72318=CONICAL_SURFACE ( 'NONE', #25865, 4.250000000000000000, 0.9599310885968754814 ) ;
#72320=ORIENTED_EDGE ( 'NONE', *, *, #53366, .T. ) ;
#72335=CARTESIAN_POINT ( 'NONE',  ( 7.500000000000000000, 1.545478204151520707, -7.491761935628703739 ) ) ;
#72380=CARTESIAN_POINT ( 'NONE',  ( -7.894787914004607998, -1.231000152045941975E-13, -7.591390474663426424 ) ) ;
#72400=ADVANCED_FACE ( 'NONE', ( #71342 ), #65478, .T. ) ;
#72489=VECTOR ( 'NONE', #76591, 1000.000000000000000 ) ;
#72517=CARTESIAN_POINT ( 'NONE',  ( -7.894706624614592272, -0.7534108004406890879, -7.590222617908723102 ) ) ;
#72526=VERTEX_POINT ( 'NONE', #78905 ) ;
#72533=CARTESIAN_POINT ( 'NONE',  ( 0.000000000000000000, 0.000000000000000000, -3.393184225085859929 ) ) ;
#72628=CARTESIAN_POINT ( 'NONE',  ( -4.250000000000000000, 5.204748896376250699E-16, -10.00000000000000000 ) ) ;
#72842=LINE ( 'NONE', #48039, #62963 ) ;
#72872=ORIENTED_EDGE ( 'NONE', *, *, #75107, .T. ) ;
#72931=VERTEX_POINT ( 'NONE', #100953 ) ;
#73025=CARTESIAN_POINT ( 'NONE',  ( 7.848314987057849024, -4.129027267381569999, -7.493854785173811095 ) ) ;
#73044=CARTESIAN_POINT ( 'NONE',  ( -7.500000000000000000, 0.7513028741560141555, -0.02472015219302758221 ) ) ;
#73082=CARTESIAN_POINT ( 'NONE',  ( 0.000000000000000000, 0.000000000000000000, -2.342872917771300578 ) ) ;
#73096=DIRECTION ( 'NONE',  ( -0.000000000000000000, -0.000000000000000000, -1.000000000000000000 ) ) ;
#73210=DIRECTION ( 'NONE',  ( -1.000000000000000000, 0.000000000000000000, 0.000000000000000000 ) ) ;
#73235=EDGE_CURVE ( 'NONE', #20907, #32853, #29747, .T. ) ;
#73275=CARTESIAN_POINT ( 'NONE',  ( 0.000000000000000000, 0.000000000000000000, -4.814498510800145681 ) ) ;
#73279=CARTESIAN_POINT ( 'NONE',  ( -4.250000000000000000, 5.204748896376250699E-16, -5.185501489199872083 ) ) ;
#73456=LINE ( 'NONE', #8734, #77319 ) ;
#73496=CARTESIAN_POINT ( 'NONE',  ( -4.999999999999998224, 5.773502691896257311, -7.063244554130002406 ) ) ;
#73538=VERTEX_POINT ( 'NONE', #3745 ) ;
#73559=DIRECTION ( 'NONE',  ( -1.000000000000000000, 0.000000000000000000, 0.000000000000000000 ) ) ;
#73566=ORIENTED_EDGE ( 'NONE', *, *, #45819, .F. ) ;
#73592=ADVANCED_FACE ( 'NONE', ( #94350 ), #17446, .F. ) ;
#73595=ORIENTED_EDGE ( 'NONE', *, *, #103079, .F. ) ;
#73610=DIRECTION ( 'NONE',  ( 1.000000000000000000, 0.000000000000000000, 0.000000000000000000 ) ) ;
#73625=DIRECTION ( 'NONE',  ( 0.8191520442889975717, 1.003171929053531773E-16, -0.5735764363510378328 ) ) ;
#73751=DIRECTION ( 'NONE',  ( -0.8191520442889884679, 1.003171929053520679E-16, 0.5735764363510508224 ) ) ;
#73769=CARTESIAN_POINT ( 'NONE',  ( -4.250000000000000000, 5.204748896376250699E-16, -6.235812796514431433 ) ) ;
#73786=CARTESIAN_POINT ( 'NONE',  ( -4.981862520314373377, 6.112127992515964325E-16, -0.01270000000000090501 ) ) ;
#73841=VECTOR ( 'NONE', #30, 1000.000000000000000 ) ;
#73843=ORIENTED_EDGE ( 'NONE', *, *, #101333, .T. ) ;
#73906=ADVANCED_FACE ( 'NONE', ( #82394 ), #45019, .F. ) ;
#73983=EDGE_LOOP ( 'NONE', ( #5299, #83061, #90541, #79724 ) ) ;
#74096=CARTESIAN_POINT ( 'NONE',  ( 2.558993250141107456, -7.638875775591494666, -7.593821156097297020 ) ) ;
#74098=CARTESIAN_POINT ( 'NONE',  ( -7.922798540899431252, 4.627424769998830456, -8.057412477672047046 ) ) ;
#74115=FACE_OUTER_BOUND ( 'NONE', #87084, .T. ) ;
#74198=DIRECTION ( 'NONE',  ( -0.000000000000000000, -0.000000000000000000, 1.000000000000000000 ) ) ;
#74213=CARTESIAN_POINT ( 'NONE',  ( -1.306442393143578240, -8.377108146505396036, -7.792327460285862983 ) ) ;
#74289=DIRECTION ( 'NONE',  ( 0.000000000000000000, 0.000000000000000000, 1.000000000000000000 ) ) ;
#74327=EDGE_CURVE ( 'NONE', #26769, #48423, #67156, .T. ) ;
#74347=CARTESIAN_POINT ( 'NONE',  ( 0.000000000000000000, 0.000000000000000000, -0.01270000000000090501 ) ) ;
#74409=CARTESIAN_POINT ( 'NONE',  ( -6.250000000000000888, -5.051814855409237026, -7.198902722707430257 ) ) ;
#74459=CARTESIAN_POINT ( 'NONE',  ( 6.601567268551443490, -5.319966374295975520, -7.792327460285858542 ) ) ;
#74470=FACE_OUTER_BOUND ( 'NONE', #65485, .T. ) ;
#74609=DIRECTION ( 'NONE',  ( -1.000000000000000000, 0.000000000000000000, 0.000000000000000000 ) ) ;
#74626=CARTESIAN_POINT ( 'NONE',  ( 6.486836893982499852, -4.915077010914404632, -7.231838333420563814 ) ) ;
#74629=CARTESIAN_POINT ( 'NONE',  ( -7.908228835406298174, 3.123118350875301985, -7.776694659840482693 ) ) ;
#74692=CARTESIAN_POINT ( 'NONE',  ( 0.000000000000000000, 0.000000000000000000, -3.764187203485586330 ) ) ;
#74734=LINE ( 'NONE', #25723, #66895 ) ;
#74789=ORIENTED_EDGE ( 'NONE', *, *, #67199, .F. ) ;
#74896=EDGE_CURVE ( 'NONE', #93010, #84586, #37091, .T. ) ;
#75037=VERTEX_POINT ( 'NONE', #7313 ) ;
#75089=DIRECTION ( 'NONE',  ( -0.000000000000000000, -0.000000000000000000, -1.000000000000000000 ) ) ;
#75107=EDGE_CURVE ( 'NONE', #64087, #94271, #76163, .T. ) ;
#75156=CARTESIAN_POINT ( 'NONE',  ( 4.419133455865365434, -6.108866147515648493, -7.026396753507436976 ) ) ;
#75351=CARTESIAN_POINT ( 'NONE',  ( -2.387978478800934834, -7.281554020289646267, -7.069802615102040555 ) ) ;
#75393=( BOUNDED_SURFACE ( )  B_SPLINE_SURFACE ( 3, 2, ( 
 ( #15543, #13945, #79751 ),
 ( #38783, #48437, #104556 ),
 ( #51631, #58679, #84549 ),
 ( #84007, #25824, #101266 ),
 ( #913, #91581, #92626 ),
 ( #33352, #43552, #68369 ),
 ( #10114, #1472, #33892 ),
 ( #34436, #42478, #75913 ) ),
 .UNSPECIFIED., .F., .F., .F. ) 
 B_SPLINE_SURFACE_WITH_KNOTS ( ( 4, 2, 2, 4 ),
 ( 3, 3 ),
 ( 0.03861844051980969916, 0.04325213341840641879, 0.04556897986770477860, 0.04788582631700313841 ),
 ( 0.000000000000000000, 1.000000000000000000 ),
 .UNSPECIFIED. ) 
 GEOMETRIC_REPRESENTATION_ITEM ( )  RATIONAL_B_SPLINE_SURFACE ( (
 ( 1.000000000000000000, 0.8047781759831923454, 1.000000000000000000),
 ( 1.000000000000000000, 0.8123762462799783979, 1.000000000000000000),
 ( 1.000000000000000000, 0.8190659850623762672, 1.000000000000000000),
 ( 1.000000000000000000, 0.8191937571010124985, 1.000000000000000000),
 ( 1.000000000000000000, 0.8176092952778098999, 1.000000000000000000),
 ( 1.000000000000000000, 0.8122962088598847386, 1.000000000000000000),
 ( 1.000000000000000000, 0.8086311330826182475, 1.000000000000000000),
 ( 1.000000000000000000, 0.8047712282214326551, 1.000000000000000000) ) ) 
 REPRESENTATION_ITEM ( '' )  SURFACE ( )  );
#75452=ORIENTED_EDGE ( 'NONE', *, *, #95120, .T. ) ;
#75480=CARTESIAN_POINT ( 'NONE',  ( 2.503857664561936320E-16, -8.660254037844401509, -7.422398894150040505 ) ) ;
#75483=EDGE_CURVE ( 'NONE', #29730, #90336, #22371, .T. ) ;
#75500=DIRECTION ( 'NONE',  ( -1.000000000000000000, 0.000000000000000000, 0.000000000000000000 ) ) ;
#75584=CARTESIAN_POINT ( 'NONE',  ( -4.174999999999998934, 5.112900386440198549E-16, -0.5776712190230098853 ) ) ;
#75631=FACE_OUTER_BOUND ( 'NONE', #57536, .T. ) ;
#75707=VERTEX_POINT ( 'NONE', #51371 ) ;
#75784=CONICAL_SURFACE ( 'NONE', #29328, 4.174999999999998934, 0.9599310885968824758 ) ;
#75832=ADVANCED_FACE ( 'NONE', ( #46480 ), #71796, .F. ) ;
#75860=AXIS2_PLACEMENT_3D ( 'NONE', #83825, #84904, #99468 ) ;
#75906=EDGE_CURVE ( 'NONE', #69179, #104354, #34167, .T. ) ;
#75913=CARTESIAN_POINT ( 'NONE',  ( -7.970070017554209407, 4.546953124339754737, -8.057670357645356773 ) ) ;
#75943=ORIENTED_EDGE ( 'NONE', *, *, #89996, .T. ) ;
#75952=FACE_OUTER_BOUND ( 'NONE', #42061, .T. ) ;
#76039=CARTESIAN_POINT ( 'NONE',  ( -5.276765049035077482, 6.073111908730296271, -7.634085501268425666 ) ) ;
#76058=CARTESIAN_POINT ( 'NONE',  ( 1.305263714129178076, -8.377797850839296956, -7.792447862505341938 ) ) ;
#76127=CARTESIAN_POINT ( 'NONE',  ( 7.500000000000000000, -4.330127018922200755, -7.422398894150036064 ) ) ;
#76163=CIRCLE ( 'NONE', #53766, 4.250000000000000000 ) ;
#76289=LINE ( 'NONE', #90355, #12733 ) ;
#76293=CARTESIAN_POINT ( 'NONE',  ( 5.000000000000000000, 6.123233995736766282E-16, -7.131971428571428184 ) ) ;
#76331=AXIS2_PLACEMENT_3D ( 'NONE', #3733, #42577, #69528 ) ;
#76416=CARTESIAN_POINT ( 'NONE',  ( 0.04725809328185524155, -9.175759667312531676, -8.057670357645365655 ) ) ;
#76581=CARTESIAN_POINT ( 'NONE',  ( 5.000000000000000000, 6.123233995736766282E-16, -7.131971428571428184 ) ) ;
#76591=DIRECTION ( 'NONE',  ( -0.8191520442889975717, 0.000000000000000000, -0.5735764363510378328 ) ) ;
#76630=ADVANCED_FACE ( 'NONE', ( #32541 ), #54912, .F. ) ;
#76672=CONICAL_SURFACE ( 'NONE', #59521, 5.000000000000000000, 0.9599310885968804774 ) ;
#76765=CARTESIAN_POINT ( 'NONE',  ( 5.047120108843204278, -5.746297884371397657, -0.1007566405101845003 ) ) ;
#76777=CARTESIAN_POINT ( 'NONE',  ( 5.274401269815139237, 6.074457022762083547, -7.633824513837112136 ) ) ;
#76794=CARTESIAN_POINT ( 'NONE',  ( 7.894787914004607998, 1.238680740843649375E-13, -7.591390474663426424 ) ) ;
#76808=VERTEX_POINT ( 'NONE', #69150 ) ;
#76855=CIRCLE ( 'NONE', #20100, 4.250000000000000000 ) ;
#76947=CIRCLE ( 'NONE', #40750, 4.250000000000000000 ) ;
#76955=CARTESIAN_POINT ( 'NONE',  ( -0.3875187462267188354, -8.436519985397220367, -7.781689322728342795 ) ) ;
#77032=CARTESIAN_POINT ( 'NONE',  ( 5.000000000000000888, 0.000000000000000000, -25.03750572909317285 ) ) ;
#77051=ORIENTED_EDGE ( 'NONE', *, *, #101780, .F. ) ;
#77109=ADVANCED_FACE ( 'NONE', ( #1583 ), #18857, .T. ) ;
#77147=CARTESIAN_POINT ( 'NONE',  ( 2.503857664561936320E-16, -8.660254037844401509, -7.422398894150040505 ) ) ;
#77248=ORIENTED_EDGE ( 'NONE', *, *, #81590, .T. ) ;
#77276=FACE_OUTER_BOUND ( 'NONE', #36803, .T. ) ;
#77319=VECTOR ( 'NONE', #66444, 1000.000000000000000 ) ;
#77402=CARTESIAN_POINT ( 'NONE',  ( 0.000000000000000000, 0.000000000000000000, -9.449444346342716017 ) ) ;
#77485=EDGE_CURVE ( 'NONE', #95526, #27550, #100039, .T. ) ;
#77497=AXIS2_PLACEMENT_3D ( 'NONE', #82671, #75089, #8776 ) ;
#77511=CARTESIAN_POINT ( 'NONE',  ( -7.703920929261754758, 4.447860822324860131, -7.917989418073283048 ) ) ;
#77543=ORIENTED_EDGE ( 'NONE', *, *, #92073, .F. ) ;
#77560=DIRECTION ( 'NONE',  ( 1.000000000000000000, 0.000000000000000000, 0.000000000000000000 ) ) ;
#77573=VERTEX_POINT ( 'NONE', #26730 ) ;
#77588=EDGE_CURVE ( 'NONE', #87281, #104590, #92475, .T. ) ;
#77608=EDGE_CURVE ( 'NONE', #65192, #55329, #35348, .T. ) ;
#77659=DIRECTION ( 'NONE',  ( 0.8191520442889884679, 0.000000000000000000, 0.5735764363510508224 ) ) ;
#77711=CIRCLE ( 'NONE', #51821, 5.000000000000000000 ) ;
#77732=CARTESIAN_POINT ( 'NONE',  ( -4.250000000000000000, 5.204748896376250699E-16, -4.814498510800145681 ) ) ;
#77740=CARTESIAN_POINT ( 'NONE',  ( 7.500000000000000888, -2.886751345948136205, -7.198902722707429369 ) ) ;
#77793=ORIENTED_EDGE ( 'NONE', *, *, #40757, .T. ) ;
#77794=ADVANCED_FACE ( 'NONE', ( #103762 ), #75784, .F. ) ;
#77851=EDGE_CURVE ( 'NONE', #12410, #17858, #15278, .T. ) ;
#77852=CARTESIAN_POINT ( 'NONE',  ( 6.602753909532903975, 5.319290460493536266, -7.792447862505333056 ) ) ;
#77861=CYLINDRICAL_SURFACE ( 'NONE', #80818, 4.250000000000000000 ) ;
#77900=EDGE_CURVE ( 'NONE', #10075, #34113, #40844, .T. ) ;
#77919=EDGE_CURVE ( 'NONE', #67329, #27550, #67174, .T. ) ;
#77995=EDGE_LOOP ( 'NONE', ( #48863, #19662, #90540, #87570 ) ) ;
#78025=CARTESIAN_POINT ( 'NONE',  ( 0.2791032213812772445, -8.821394357840576461, -7.929128246061912577 ) ) ;
#78052=EDGE_CURVE ( 'NONE', #106311, #54954, #17211, .T. ) ;
#78080=CARTESIAN_POINT ( 'NONE',  ( 0.000000000000000000, 0.000000000000000000, -8.500000000000000000 ) ) ;
#78172=CIRCLE ( 'NONE', #93675, 4.250000000000000000 ) ;
#78308=ORIENTED_EDGE ( 'NONE', *, *, #75107, .F. ) ;
#78323=AXIS2_PLACEMENT_3D ( 'NONE', #51745, #25942, #33469 ) ;
#78440=EDGE_CURVE ( 'NONE', #27550, #67329, #19017, .T. ) ;
#78458=AXIS2_PLACEMENT_3D ( 'NONE', #31513, #90786, #105374 ) ;
#78460=CARTESIAN_POINT ( 'NONE',  ( -2.352990130084491319E-16, 8.660254037844390851, -10.00000000000000000 ) ) ;
#78523=EDGE_CURVE ( 'NONE', #37257, #104590, #30557, .T. ) ;
#78557=CARTESIAN_POINT ( 'NONE',  ( -7.894787914004607998, -1.231000152045941975E-13, -7.591390474663426424 ) ) ;
#78603=B_SPLINE_CURVE_WITH_KNOTS ( 'NONE', 3,
 ( #84245, #68055, #20635, #43781, #42721, #18470 ),
 .UNSPECIFIED., .F., .F.,
 ( 4, 2, 4 ),
 ( 0.004444412883774349725, 0.006655097293744438938, 0.008865781703714527284 ),
 .UNSPECIFIED. ) ;
#78648=LINE ( 'NONE', #61983, #72052 ) ;
#78682=CARTESIAN_POINT ( 'NONE',  ( -1.908195823574487804E-14, -8.660254037844390851, -0.9999999999999974465 ) ) ;
#78759=B_SPLINE_CURVE_WITH_KNOTS ( 'NONE', 3,
 ( #72380, #15738, #48621, #39506, #57242, #31433 ),
 .UNSPECIFIED., .F., .F.,
 ( 4, 2, 4 ),
 ( 0.004615310220740755608, 0.006918661718823359771, 0.009222013216905963068 ),
 .UNSPECIFIED. ) ;
#78812=SURFACE_STYLE_FILL_AREA ( #70202 ) ;
#78866=EDGE_CURVE ( 'NONE', #32369, #83574, #103682, .T. ) ;
#78905=CARTESIAN_POINT ( 'NONE',  ( 5.000000000000000000, 6.123233995736766282E-16, -9.974599999999998801 ) ) ;
#78997=ORIENTED_EDGE ( 'NONE', *, *, #16736, .F. ) ;
#79046=CARTESIAN_POINT ( 'NONE',  ( 5.000000000000000000, 6.123233995736766282E-16, -1.446714285714285841 ) ) ;
#79154=ORIENTED_EDGE ( 'NONE', *, *, #79320, .F. ) ;
#79193=CARTESIAN_POINT ( 'NONE',  ( 7.703928834700302986, 4.447865386531935528, -7.917997657324739258 ) ) ;
#79198=DIRECTION ( 'NONE',  ( 0.8191520442889975717, 1.003171929053531773E-16, -0.5735764363510378328 ) ) ;
#79227=EDGE_CURVE ( 'NONE', #72526, #84586, #31163, .T. ) ;
#79243=CARTESIAN_POINT ( 'NONE',  ( 2.621328321947801854, 7.606199919103181273, -7.633618187056858240 ) ) ;
#79259=ORIENTED_EDGE ( 'NONE', *, *, #53898, .T. ) ;
#79320=EDGE_CURVE ( 'NONE', #83574, #9383, #71792, .T. ) ;
#79324=ORIENTED_EDGE ( 'NONE', *, *, #28654, .T. ) ;
#79370=CARTESIAN_POINT ( 'NONE',  ( 0.000000000000000000, 0.000000000000000000, -0.01270000000000090501 ) ) ;
#79386=EDGE_LOOP ( 'NONE', ( #6063, #19429, #10441, #77543 ) ) ;
#79429=AXIS2_PLACEMENT_3D ( 'NONE', #48224, #97847, #73559 ) ;
#79461=LINE ( 'NONE', #29364, #13263 ) ;
#79464=EDGE_LOOP ( 'NONE', ( #18486, #59788, #51901, #11012 ) ) ;
#79484=CARTESIAN_POINT ( 'NONE',  ( 0.000000000000000000, 0.000000000000000000, -0.5776712190230098853 ) ) ;
#79540=CARTESIAN_POINT ( 'NONE',  ( 7.500000000000000000, 3.988838049906436201, -0.8529248949437627791 ) ) ;
#79561=VECTOR ( 'NONE', #25120, 1000.000000000000000 ) ;
#79600=DIRECTION ( 'NONE',  ( 0.000000000000000000, 0.000000000000000000, 1.000000000000000000 ) ) ;
#79605=( NAMED_UNIT ( * ) PLANE_ANGLE_UNIT ( ) SI_UNIT ( $, .RADIAN. ) );
#79724=ORIENTED_EDGE ( 'NONE', *, *, #55769, .T. ) ;
#79751=CARTESIAN_POINT ( 'NONE',  ( 0.04606493828584038580, 9.175055303659558348, -8.057411785091792567 ) ) ;
#79770=FACE_OUTER_BOUND ( 'NONE', #87837, .T. ) ;
#79778=EDGE_LOOP ( 'NONE', ( #31873, #24155, #46372, #87053 ) ) ;
#79977=DIRECTION ( 'NONE',  ( -1.000000000000000000, 0.000000000000000000, 0.000000000000000000 ) ) ;
#80096=CARTESIAN_POINT ( 'NONE',  ( 7.500000000000001776, -4.330127018922199866, -0.9999999999999974465 ) ) ;
#80106=DIRECTION ( 'NONE',  ( 1.000000000000000000, 0.000000000000000000, 0.000000000000000000 ) ) ;
#80227=LINE ( 'NONE', #54887, #98971 ) ;
#80228=DIRECTION ( 'NONE',  ( -1.000000000000000000, 0.000000000000000000, 0.000000000000000000 ) ) ;
#80274=AXIS2_PLACEMENT_3D ( 'NONE', #82824, #42362, #8923 ) ;
#80290=CARTESIAN_POINT ( 'NONE',  ( 2.411464220262822256, 7.267994521134540697, -7.491772860716854332 ) ) ;
#80385=CARTESIAN_POINT ( 'NONE',  ( 7.894787914004607998, 1.238680740843649375E-13, -7.591390474663426424 ) ) ;
#80561=AXIS2_PLACEMENT_3D ( 'NONE', #29004, #96349, #86676 ) ;
#80592=CARTESIAN_POINT ( 'NONE',  ( 7.500000000000000888, 0.000000000000000000, 1.734723475976807094E-15 ) ) ;
#80600=CARTESIAN_POINT ( 'NONE',  ( -7.499999999999998224, -1.545780083833950380, -7.491787297939224821 ) ) ;
#80623=DIRECTION ( 'NONE',  ( -1.000000000000000000, 0.000000000000000000, 0.000000000000000000 ) ) ;
#80642=CARTESIAN_POINT ( 'NONE',  ( 0.000000000000000000, 0.000000000000000000, -7.131971428571428184 ) ) ;
#80665=B_SPLINE_CURVE_WITH_KNOTS ( 'NONE', 3,
 ( #51952, #59005, #91891, #76765, #100509, #3424 ),
 .UNSPECIFIED., .F., .F.,
 ( 4, 2, 4 ),
 ( 2.475503369175507341E-07, 0.002222330217055621098, 0.004444412883774324571 ),
 .UNSPECIFIED. ) ;
#80670=DIRECTION ( 'NONE',  ( 1.000000000000000000, 0.000000000000000000, 0.000000000000000000 ) ) ;
#80765=DIRECTION ( 'NONE',  ( -0.000000000000000000, 0.000000000000000000, -1.000000000000000000 ) ) ;
#80781=DIRECTION ( 'NONE',  ( -0.8191520442889975717, 0.000000000000000000, -0.5735764363510378328 ) ) ;
#80818=AXIS2_PLACEMENT_3D ( 'NONE', #86515, #28829, #43892 ) ;
#80858=ADVANCED_FACE ( 'NONE', ( #18057 ), #53526, .F. ) ;
#80861=VECTOR ( 'NONE', #38975, 1000.000000000000000 ) ;
#80875=CARTESIAN_POINT ( 'NONE',  ( 10.39117206796836257, 1.272551561242683764E-15, -8.500000000000000000 ) ) ;
#80950=DIRECTION ( 'NONE',  ( 1.000000000000000000, 0.000000000000000000, 0.000000000000000000 ) ) ;
#80966=EDGE_LOOP ( 'NONE', ( #48805, #58909, #100363, #36812, #50114 ) ) ;
#81070=EDGE_CURVE ( 'NONE', #54954, #106311, #77711, .T. ) ;
#81265=DIRECTION ( 'NONE',  ( -1.000000000000000000, 0.000000000000000000, 0.000000000000000000 ) ) ;
#81273=ORIENTED_EDGE ( 'NONE', *, *, #89354, .T. ) ;
#81297=DIRECTION ( 'NONE',  ( -0.8191520442889975717, 0.000000000000000000, -0.5735764363510378328 ) ) ;
#81321=DIRECTION ( 'NONE',  ( -1.000000000000000000, 0.000000000000000000, 0.000000000000000000 ) ) ;
#81366=DIRECTION ( 'NONE',  ( 1.000000000000000000, 0.000000000000000000, 0.000000000000000000 ) ) ;
#81380=EDGE_CURVE ( 'NONE', #90212, #59052, #30269, .T. ) ;
#81388=VERTEX_POINT ( 'NONE', #44862 ) ;
#81409=ORIENTED_EDGE ( 'NONE', *, *, #84349, .F. ) ;
#81450=SHAPE_REPRESENTATION_RELATIONSHIP ( 'NONE' , 'NONE' ,  #7490, #44833 ) ;
#81590=EDGE_CURVE ( 'NONE', #18346, #87281, #100915, .T. ) ;
#81643=CARTESIAN_POINT ( 'NONE',  ( 6.625705691649121931, -5.306270977113076270, -7.795653906408811729 ) ) ;
#81646=CARTESIAN_POINT ( 'NONE',  ( -7.500000000000000000, -4.732323933430413909, -7.493854309896103238 ) ) ;
#81667=VERTEX_POINT ( 'NONE', #9141 ) ;
#81689=DIRECTION ( 'NONE',  ( 0.000000000000000000, 0.000000000000000000, 1.000000000000000000 ) ) ;
#81704=DIRECTION ( 'NONE',  ( -1.000000000000000000, 0.000000000000000000, 0.000000000000000000 ) ) ;
#81781=CARTESIAN_POINT ( 'NONE',  ( 0.000000000000000000, 0.000000000000000000, 0.000000000000000000 ) ) ;
#81883=FACE_OUTER_BOUND ( 'NONE', #94555, .T. ) ;
#81933=DIRECTION ( 'NONE',  ( 0.000000000000000000, 0.000000000000000000, 1.000000000000000000 ) ) ;
#82028=LINE ( 'NONE', #66389, #57714 ) ;
#82033=VECTOR ( 'NONE', #57698, 1000.000000000000000 ) ;
#82188=CARTESIAN_POINT ( 'NONE',  ( 7.779103221381273414, -4.168986698926031131, -7.929128246061905472 ) ) ;
#82209=AXIS2_PLACEMENT_3D ( 'NONE', #1631, #25437, #65327 ) ;
#82359=VERTEX_POINT ( 'NONE', #45145 ) ;
#82394=FACE_OUTER_BOUND ( 'NONE', #53408, .T. ) ;
#82403=DIRECTION ( 'NONE',  ( -0.8191520442889884679, 1.003171929053520679E-16, 0.5735764363510508224 ) ) ;
#82414=CARTESIAN_POINT ( 'NONE',  ( 0.000000000000000000, 0.000000000000000000, -1.971869939371574620 ) ) ;
#82420=CARTESIAN_POINT ( 'NONE',  ( 0.000000000000000000, 0.000000000000000000, -10.00000000000000000 ) ) ;
#82456=FACE_OUTER_BOUND ( 'NONE', #3384, .T. ) ;
#82487=CYLINDRICAL_SURFACE ( 'NONE', #15616, 4.250000000000000000 ) ;
#82551=CARTESIAN_POINT ( 'NONE',  ( 7.500000000000000000, 4.732328341851994580, -7.493855119309152713 ) ) ;
#82577=DIRECTION ( 'NONE',  ( 1.000000000000000000, 0.000000000000000000, 0.000000000000000000 ) ) ;
#82671=CARTESIAN_POINT ( 'NONE',  ( 0.000000000000000000, 0.000000000000000000, -1.446714285714285841 ) ) ;
#82769=DIRECTION ( 'NONE',  ( -0.000000000000000000, -0.000000000000000000, -1.000000000000000000 ) ) ;
#82821=CARTESIAN_POINT ( 'NONE',  ( -7.500000000000000000, -4.330127018922203419, -0.9999999999999974465 ) ) ;
#82824=CARTESIAN_POINT ( 'NONE',  ( 0.000000000000000000, 0.000000000000000000, 1.734723475976807094E-15 ) ) ;
#82923=CARTESIAN_POINT ( 'NONE',  ( -7.777900015783948184, -4.169681370001537601, -7.928862157988302073 ) ) ;
#82994=CARTESIAN_POINT ( 'NONE',  ( 5.000000000000000000, 6.123233995736766282E-16, -4.289342857142857568 ) ) ;
#83008=CARTESIAN_POINT ( 'NONE',  ( -6.318250223874061420E-16, 9.147862274876551680, -8.047472243342934206 ) ) ;
#83061=ORIENTED_EDGE ( 'NONE', *, *, #75906, .F. ) ;
#83078=ADVANCED_FACE ( 'NONE', ( #104550 ), #26323, .F. ) ;
#83195=DIRECTION ( 'NONE',  ( 0.000000000000000000, 0.000000000000000000, 1.000000000000000000 ) ) ;
#83259=CARTESIAN_POINT ( 'NONE',  ( -0.04606493828583509142, -9.175055303659565453, -8.057411785091796119 ) ) ;
#83281=CARTESIAN_POINT ( 'NONE',  ( 5.000000000000000000, 6.123233995736766282E-16, -0.02540000000000007530 ) ) ;
#83347=CARTESIAN_POINT ( 'NONE',  ( -7.499999999999999112, -2.930060224340427677, -0.4701183149080218060 ) ) ;
#83379=EDGE_CURVE ( 'NONE', #48423, #67329, #67299, .T. ) ;
#83415=CARTESIAN_POINT ( 'NONE',  ( 3.749999999999999112, 6.495190528383288253, -6.991905250253753756 ) ) ;
#83423=ORIENTED_EDGE ( 'NONE', *, *, #81380, .F. ) ;
#83448=CARTESIAN_POINT ( 'NONE',  ( -6.523606932384105939, -4.893847819345124250, -7.213065638946083880 ) ) ;
#83566=CARTESIAN_POINT ( 'NONE',  ( 5.000000000000000000, 6.123233995736766282E-16, -4.289342857142857568 ) ) ;
#83574=VERTEX_POINT ( 'NONE', #78557 ) ;
#83595=CARTESIAN_POINT ( 'NONE',  ( -2.623433461001182021, 7.604994000793857012, -7.633824513837113024 ) ) ;
#83625=CIRCLE ( 'NONE', #30308, 10.12668159690567649 ) ;
#83825=CARTESIAN_POINT ( 'NONE',  ( 0.000000000000000000, 0.000000000000000000, -4.814498510800145681 ) ) ;
#83904=ORIENTED_EDGE ( 'NONE', *, *, #77608, .F. ) ;
#83920=CIRCLE ( 'NONE', #51250, 4.250000000000000000 ) ;
#83941=FACE_OUTER_BOUND ( 'NONE', #96681, .T. ) ;
#83956=EDGE_LOOP ( 'NONE', ( #46887, #24037, #40015, #49796 ) ) ;
#84007=CARTESIAN_POINT ( 'NONE',  ( -4.419133455862510829, 6.108866147517284517, -7.026396753507433424 ) ) ;
#84078=EDGE_CURVE ( 'NONE', #66630, #45380, #88403, .T. ) ;
#84087=B_SPLINE_CURVE_WITH_KNOTS ( 'NONE', 3,
 ( #80592, #5654, #22932, #38576, #21877, #14798, #87653, #31034, #79540, #47693 ),
 .UNSPECIFIED., .F., .F.,
 ( 4, 2, 2, 2, 4 ),
 ( 0.01051144076094937159, 0.01162027323572613347, 0.01272910571050289534, 0.01383793818527965722, 0.01494677066005641909 ),
 .UNSPECIFIED. ) ;
#84122=CONICAL_SURFACE ( 'NONE', #66883, 7.500000000000000888, 0.8594454914424817238 ) ;
#84245=CARTESIAN_POINT ( 'NONE',  ( -3.750000000000004441, -6.495190528383288253, 1.734723475976807094E-15 ) ) ;
#84349=EDGE_CURVE ( 'NONE', #26769, #65192, #65985, .T. ) ;
#84381=EDGE_CURVE ( 'NONE', #32853, #75707, #99353, .T. ) ;
#84396=DIRECTION ( 'NONE',  ( -1.000000000000000000, 0.000000000000000000, 0.000000000000000000 ) ) ;
#84401=CARTESIAN_POINT ( 'NONE',  ( 2.503857664561936320E-16, -8.660254037844401509, -10.00000000000000000 ) ) ;
#84407=DIRECTION ( 'NONE',  ( -0.000000000000000000, -0.000000000000000000, -1.000000000000000000 ) ) ;
#84489=ORIENTED_EDGE ( 'NONE', *, *, #46317, .T. ) ;
#84501=EDGE_LOOP ( 'NONE', ( #40437, #56870, #48876, #58593 ) ) ;
#84549=CARTESIAN_POINT ( 'NONE',  ( -2.558993250146713638, 7.638875775588015671, -7.593821156097209979 ) ) ;
#84586=VERTEX_POINT ( 'NONE', #94397 ) ;
#84589=DIRECTION ( 'NONE',  ( 1.000000000000000000, 0.000000000000000000, 0.000000000000000000 ) ) ;
#84643=DIRECTION ( 'NONE',  ( -1.000000000000000000, 0.000000000000000000, 0.000000000000000000 ) ) ;
#84696=CARTESIAN_POINT ( 'NONE',  ( 4.613983237546153582, -6.452243898629819618, -7.591546097228406786 ) ) ;
#84858=DIRECTION ( 'NONE',  ( 0.8191520442889975717, 1.003171929053531773E-16, -0.5735764363510378328 ) ) ;
#84889=FACE_OUTER_BOUND ( 'NONE', #84501, .T. ) ;
#84903=CARTESIAN_POINT ( 'NONE',  ( 0.000000000000000000, 0.000000000000000000, -6.235812796514431433 ) ) ;
#84904=DIRECTION ( 'NONE',  ( 0.000000000000000000, 0.000000000000000000, 1.000000000000000000 ) ) ;
#84912=EDGE_CURVE ( 'NONE', #72931, #2343, #5772, .T. ) ;
#85183=DIRECTION ( 'NONE',  ( -1.000000000000000000, 0.000000000000000000, 0.000000000000000000 ) ) ;
#85295=DIRECTION ( 'NONE',  ( 1.000000000000000000, 0.000000000000000000, 0.000000000000000000 ) ) ;
#85347=EDGE_LOOP ( 'NONE', ( #60957, #100537, #77793, #89532 ) ) ;
#85408=ORIENTED_EDGE ( 'NONE', *, *, #79227, .T. ) ;
#85442=EDGE_CURVE ( 'NONE', #27490, #72526, #13085, .T. ) ;
#85474=CARTESIAN_POINT ( 'NONE',  ( 0.000000000000000000, 0.000000000000000000, -7.657127082228716297 ) ) ;
#85505=LINE ( 'NONE', #78460, #92532 ) ;
#85552=AXIS2_PLACEMENT_3D ( 'NONE', #41903, #68321, #101215 ) ;
#85598=CARTESIAN_POINT ( 'NONE',  ( -4.250000000000000000, 5.204748896376250699E-16, -4.814498510800145681 ) ) ;
#85694=ORIENTED_EDGE ( 'NONE', *, *, #46317, .F. ) ;
#85697=AXIS2_PLACEMENT_3D ( 'NONE', #34734, #67605, #94412 ) ;
#85722=DIRECTION ( 'NONE',  ( -0.000000000000000000, -0.000000000000000000, -1.000000000000000000 ) ) ;
#85732=EDGE_CURVE ( 'NONE', #104354, #71702, #92827, .T. ) ;
#85847=CARTESIAN_POINT ( 'NONE',  ( 7.500000000000000000, 2.886751345948123770, -7.198902722707427593 ) ) ;
#85860=CARTESIAN_POINT ( 'NONE',  ( 6.902527771671632451, 4.675077770780898589, -0.7026937717022772034 ) ) ;
#85871=EDGE_CURVE ( 'NONE', #12410, #32853, #54069, .T. ) ;
#85968=AXIS2_PLACEMENT_3D ( 'NONE', #45559, #104294, #13688 ) ;
#86012=ORIENTED_EDGE ( 'NONE', *, *, #9885, .T. ) ;
#86112=ORIENTED_EDGE ( 'NONE', *, *, #69048, .T. ) ;
#86126=ORIENTED_EDGE ( 'NONE', *, *, #79320, .T. ) ;
#86136=FACE_OUTER_BOUND ( 'NONE', #31999, .T. ) ;
#86200=AXIS2_PLACEMENT_3D ( 'NONE', #41759, #56868, #24026 ) ;
#86222=CONICAL_SURFACE ( 'NONE', #29417, 4.250000000000000000, 0.9599310885968754814 ) ;
#86281=AXIS2_PLACEMENT_3D ( 'NONE', #62673, #56667, #80950 ) ;
#86512=CARTESIAN_POINT ( 'NONE',  ( -7.500000000000000000, -4.330127018922201643, -7.422398894150036064 ) ) ;
#86515=CARTESIAN_POINT ( 'NONE',  ( 0.000000000000000000, 0.000000000000000000, -10.00000000000000000 ) ) ;
#86567=ORIENTED_EDGE ( 'NONE', *, *, #32967, .F. ) ;
#86579=AXIS2_PLACEMENT_3D ( 'NONE', #54928, #87853, #81321 ) ;
#86676=DIRECTION ( 'NONE',  ( 1.000000000000000000, 0.000000000000000000, 0.000000000000000000 ) ) ;
#86695=DIRECTION ( 'NONE',  ( -0.8660254037844381525, 0.5000000000000007772, 0.000000000000000000 ) ) ;
#86812=CARTESIAN_POINT ( 'NONE',  ( 0.5974722283283642188, -8.315303285985693904, -0.7026937717022943009 ) ) ;
#86839=DIRECTION ( 'NONE',  ( -0.000000000000000000, -0.000000000000000000, -1.000000000000000000 ) ) ;
#86881=DIRECTION ( 'NONE',  ( -0.000000000000000000, -0.000000000000000000, -1.000000000000000000 ) ) ;
#86902=VECTOR ( 'NONE', #15537, 1000.000000000000000 ) ;
#86929=LINE ( 'NONE', #37869, #61614 ) ;
#87023=CYLINDRICAL_SURFACE ( 'NONE', #87177, 5.000000000000000888 ) ;
#87053=ORIENTED_EDGE ( 'NONE', *, *, #81590, .F. ) ;
#87082=CARTESIAN_POINT ( 'NONE',  ( 0.000000000000000000, 0.000000000000000000, -6.606815774914157835 ) ) ;
#87084=EDGE_LOOP ( 'NONE', ( #100490, #95241, #91285, #64379 ) ) ;
#87143=ORIENTED_EDGE ( 'NONE', *, *, #70530, .T. ) ;
#87162=CARTESIAN_POINT ( 'NONE',  ( -2.352990130084491319E-16, 8.660254037844390851, -7.422398894150036064 ) ) ;
#87169=ORIENTED_EDGE ( 'NONE', *, *, #7530, .T. ) ;
#87177=AXIS2_PLACEMENT_3D ( 'NONE', #93518, #95632, #21770 ) ;
#87281=VERTEX_POINT ( 'NONE', #34801 ) ;
#87345=EDGE_CURVE ( 'NONE', #65192, #75037, #65865, .T. ) ;
#87354=CARTESIAN_POINT ( 'NONE',  ( -0.3483149870578508001, 8.861353789385022495, -7.493854785173812871 ) ) ;
#87442=CARTESIAN_POINT ( 'NONE',  ( 7.500000000000000000, 4.330127018922203419, -0.9999999999999974465 ) ) ;
#87462=( LENGTH_UNIT ( ) NAMED_UNIT ( * ) SI_UNIT ( .MILLI., .METRE. ) );
#87473=ORIENTED_EDGE ( 'NONE', *, *, #3608, .F. ) ;
#87479=DIRECTION ( 'NONE',  ( 0.000000000000000000, 0.000000000000000000, 1.000000000000000000 ) ) ;
#87536=CARTESIAN_POINT ( 'NONE',  ( 5.000000000000000000, 6.123233995736766282E-16, -9.974599999999998801 ) ) ;
#87570=ORIENTED_EDGE ( 'NONE', *, *, #92045, .F. ) ;
#87653=CARTESIAN_POINT ( 'NONE',  ( 7.500000000000000888, 2.932633423934448924, -0.4709827563909285697 ) ) ;
#87685=CARTESIAN_POINT ( 'NONE',  ( -4.250000000000000000, 5.204748896376250699E-16, -1.971869939371574620 ) ) ;
#87811=ORIENTED_EDGE ( 'NONE', *, *, #17543, .T. ) ;
#87831=DIRECTION ( 'NONE',  ( -0.000000000000000000, -0.000000000000000000, -1.000000000000000000 ) ) ;
#87837=EDGE_LOOP ( 'NONE', ( #44967, #92049, #62476, #86567 ) ) ;
#87853=DIRECTION ( 'NONE',  ( -0.000000000000000000, -0.000000000000000000, -1.000000000000000000 ) ) ;
#87881=CARTESIAN_POINT ( 'NONE',  ( 3.080866544135465013, 6.881514909250465273, -7.026396753507434312 ) ) ;
#87889=CARTESIAN_POINT ( 'NONE',  ( 0.000000000000000000, 0.000000000000000000, -4.289342857142857568 ) ) ;
#87949=DIRECTION ( 'NONE',  ( -1.000000000000000000, 0.000000000000000000, 0.000000000000000000 ) ) ;
#87995=AXIS2_PLACEMENT_3D ( 'NONE', #80642, #96332, #105464 ) ;
#88004=DIRECTION ( 'NONE',  ( -0.9396926207859143121, 0.000000000000000000, -0.3420201433256525592 ) ) ;
#88156=ADVANCED_FACE ( 'NONE', ( #106706 ), #76672, .F. ) ;
#88403=CIRCLE ( 'NONE', #21296, 4.250000000000000000 ) ;
#88412=CARTESIAN_POINT ( 'NONE',  ( 4.250000000000000000, 0.000000000000000000, -6.235812796514431433 ) ) ;
#88522=DIRECTION ( 'NONE',  ( -1.000000000000000000, 0.000000000000000000, 0.000000000000000000 ) ) ;
#88615=CARTESIAN_POINT ( 'NONE',  ( 0.000000000000000000, 0.000000000000000000, -1.446714285714285841 ) ) ;
#88679=ORIENTED_EDGE ( 'NONE', *, *, #103336, .T. ) ;
#88703=ORIENTED_EDGE ( 'NONE', *, *, #95099, .F. ) ;
#88792=EDGE_CURVE ( 'NONE', #4416, #23008, #59678, .T. ) ;
#88799=ADVANCED_FACE ( 'NONE', ( #58004 ), #37296, .T. ) ;
#88909=AXIS2_PLACEMENT_3D ( 'NONE', #95275, #79600, #38637 ) ;
#88911=AXIS2_PLACEMENT_3D ( 'NONE', #26106, #49245, #50835 ) ;
#88997=CARTESIAN_POINT ( 'NONE',  ( -6.318250223874061420E-16, 9.147862274876551680, -8.047472243342934206 ) ) ;
#89073=CIRCLE ( 'NONE', #82209, 4.250000000000000000 ) ;
#89207=CIRCLE ( 'NONE', #56460, 7.500000000000003553 ) ;
#89244=CARTESIAN_POINT ( 'NONE',  ( 7.169303301815730833, -4.521054846639009916, -7.349897473154584304 ) ) ;
#89269=CARTESIAN_POINT ( 'NONE',  ( 7.500000000000000000, -3.640541674360520119, -0.7158139487964582104 ) ) ;
#89270=DIRECTION ( 'NONE',  ( -0.000000000000000000, -0.000000000000000000, -1.000000000000000000 ) ) ;
#89354=EDGE_CURVE ( 'NONE', #45380, #66630, #30975, .T. ) ;
#89397=EDGE_LOOP ( 'NONE', ( #66914, #86112, #57517, #48980 ) ) ;
#89451=CARTESIAN_POINT ( 'NONE',  ( 0.000000000000000000, 8.660254037844390851, -0.9999999999999974465 ) ) ;
#89478=ORIENTED_EDGE ( 'NONE', *, *, #42810, .T. ) ;
#89532=ORIENTED_EDGE ( 'NONE', *, *, #77919, .F. ) ;
#89579=EDGE_CURVE ( 'NONE', #69179, #49340, #78648, .T. ) ;
#89674=ADVANCED_FACE ( 'NONE', ( #55953 ), #3222, .F. ) ;
#89734=ADVANCED_FACE ( 'NONE', ( #41392 ), #6673, .F. ) ;
#89741=EDGE_CURVE ( 'NONE', #26814, #67329, #33327, .T. ) ;
#89888=( BOUNDED_SURFACE ( )  B_SPLINE_SURFACE ( 3, 2, ( 
 ( #32805, #82923, #41929 ),
 ( #83448, #66744, #34416 ),
 ( #1993, #59730, #50535 ),
 ( #42459, #24714, #92606 ),
 ( #75351, #18217, #51068 ),
 ( #34940, #67810, #45664 ),
 ( #93687, #76955, #35477 ),
 ( #44610, #78025, #76416 ) ),
 .UNSPECIFIED., .F., .F., .F. ) 
 B_SPLINE_SURFACE_WITH_KNOTS ( ( 4, 2, 2, 4 ),
 ( 3, 3 ),
 ( 0.03861844051980970610, 0.04325213341840641879, 0.04556897986770477860, 0.04788582631700313841 ),
 ( 0.000000000000000000, 1.000000000000000000 ),
 .UNSPECIFIED. ) 
 GEOMETRIC_REPRESENTATION_ITEM ( )  RATIONAL_B_SPLINE_SURFACE ( (
 ( 1.000000000000000000, 0.8047781759831924564, 1.000000000000000000),
 ( 1.000000000000000000, 0.8123762462804489104, 1.000000000000000000),
 ( 1.000000000000000000, 0.8190659850617495463, 1.000000000000000000),
 ( 1.000000000000000000, 0.8191937571013252484, 1.000000000000000000),
 ( 1.000000000000000000, 0.8176092952780751322, 1.000000000000000000),
 ( 1.000000000000000000, 0.8122962088596183960, 1.000000000000000000),
 ( 1.000000000000000000, 0.8086311330828166444, 1.000000000000000000),
 ( 1.000000000000000000, 0.8047712282214323221, 1.000000000000000000) ) ) 
 REPRESENTATION_ITEM ( '' )  SURFACE ( )  );
#89974=CARTESIAN_POINT ( 'NONE',  ( -3.096526599377911193, 6.872473572140713749, 2.349104707051923644E-15 ) ) ;
#89986=CARTESIAN_POINT ( 'NONE',  ( 7.703928834700305650, -4.447865386531949738, -7.917997657324739258 ) ) ;
#89996=EDGE_CURVE ( 'NONE', #94271, #4153, #37064, .T. ) ;
#90003=CIRCLE ( 'NONE', #21380, 7.500000000000000888 ) ;
#90082=VECTOR ( 'NONE', #9095, 1000.000000000000000 ) ;
#90093=CARTESIAN_POINT ( 'NONE',  ( 7.500000000000001776, -4.330127018922199866, -0.9999999999999974465 ) ) ;
#90181=ORIENTED_EDGE ( 'NONE', *, *, #83379, .T. ) ;
#90212=VERTEX_POINT ( 'NONE', #6774 ) ;
#90293=CARTESIAN_POINT ( 'NONE',  ( 2.325424218456834335, -7.317669739338271917, -7.030005583190792606 ) ) ;
#90296=CARTESIAN_POINT ( 'NONE',  ( -7.500000000000000000, 4.730921838224019460, -7.493596905200499592 ) ) ;
#90336=VERTEX_POINT ( 'NONE', #62138 ) ;
#90355=CARTESIAN_POINT ( 'NONE',  ( 4.250000000000000000, 0.000000000000000000, -1.971869939371574620 ) ) ;
#90386=AXIS2_PLACEMENT_3D ( 'NONE', #61235, #94119, #61780 ) ;
#90402=CARTESIAN_POINT ( 'NONE',  ( 0.000000000000000000, 0.000000000000000000, 0.000000000000000000 ) ) ;
#90540=ORIENTED_EDGE ( 'NONE', *, *, #93433, .F. ) ;
#90541=ORIENTED_EDGE ( 'NONE', *, *, #96554, .T. ) ;
#90770=DIRECTION ( 'NONE',  ( -1.000000000000000000, 0.000000000000000000, 0.000000000000000000 ) ) ;
#90786=DIRECTION ( 'NONE',  ( 0.000000000000000000, 0.000000000000000000, 1.000000000000000000 ) ) ;
#90789=ORIENTED_EDGE ( 'NONE', *, *, #19217, .F. ) ;
#90796=CARTESIAN_POINT ( 'NONE',  ( -5.000000000000000000, 0.000000000000000000, -2.868028571428571372 ) ) ;
#90837=CARTESIAN_POINT ( 'NONE',  ( -7.500000000000000000, -4.652405105468744750, -7.929127756970858698 ) ) ;
#90853=CIRCLE ( 'NONE', #44351, 4.250000000000000000 ) ;
#90871=CARTESIAN_POINT ( 'NONE',  ( 7.907996613752301229, 3.055722423191984838, -7.792112796859424151 ) ) ;
#90927=CONICAL_SURFACE ( 'NONE', #44430, 5.000000000000000000, 0.9599310885968804774 ) ;
#90960=AXIS2_PLACEMENT_3D ( 'NONE', #96959, #63547, #80228 ) ;
#91017=EDGE_CURVE ( 'NONE', #77573, #62254, #43100, .T. ) ;
#91124=DIRECTION ( 'NONE',  ( -1.000000000000000000, 0.000000000000000000, 0.000000000000000000 ) ) ;
#91233=CARTESIAN_POINT ( 'NONE',  ( -5.000000000000000000, 0.000000000000000000, -1.446714285714285841 ) ) ;
#91271=DIRECTION ( 'NONE',  ( -0.000000000000000000, -0.000000000000000000, -1.000000000000000000 ) ) ;
#91285=ORIENTED_EDGE ( 'NONE', *, *, #88792, .F. ) ;
#91388=CARTESIAN_POINT ( 'NONE',  ( 3.280815508853482942, 7.221948645665444921, -7.591546097228403234 ) ) ;
#91447=CARTESIAN_POINT ( 'NONE',  ( 3.750000000000000888, -6.495190528383301576, -6.991905250253759085 ) ) ;
#91534=ORIENTED_EDGE ( 'NONE', *, *, #85442, .F. ) ;
#91572=ORIENTED_EDGE ( 'NONE', *, *, #27802, .T. ) ;
#91581=CARTESIAN_POINT ( 'NONE',  ( -5.088535779736856668, 5.722386535631781790, -7.491772860716145566 ) ) ;
#91657=EDGE_CURVE ( 'NONE', #60305, #11929, #27677, .T. ) ;
#91741=VERTEX_POINT ( 'NONE', #96086 ) ;
#91832=CARTESIAN_POINT ( 'NONE',  ( -2.500000000000000000, 7.216878364870323637, -7.063244554130002406 ) ) ;
#91891=CARTESIAN_POINT ( 'NONE',  ( 6.293430271071538407, -5.026740376715103764, -0.4524126574264524248 ) ) ;
#91959=AXIS2_PLACEMENT_3D ( 'NONE', #73082, #9411, #84396 ) ;
#91962=CARTESIAN_POINT ( 'NONE',  ( 6.874999999999996447, -4.690970937165717558, -7.298562697733106397 ) ) ;
#92004=CARTESIAN_POINT ( 'NONE',  ( -6.293430271071535742, 5.026740376715093106, -0.4524126574264451528 ) ) ;
#92045=EDGE_CURVE ( 'NONE', #38530, #30487, #50682, .T. ) ;
#92049=ORIENTED_EDGE ( 'NONE', *, *, #9325, .F. ) ;
#92051=DIRECTION ( 'NONE',  ( -1.000000000000000000, 0.000000000000000000, 0.000000000000000000 ) ) ;
#92072=FACE_OUTER_BOUND ( 'NONE', #79778, .T. ) ;
#92073=EDGE_CURVE ( 'NONE', #4416, #76808, #102453, .T. ) ;
#92133=FACE_OUTER_BOUND ( 'NONE', #1411, .T. ) ;
#92298=CIRCLE ( 'NONE', #66511, 4.250000000000000000 ) ;
#92348=CARTESIAN_POINT ( 'NONE',  ( -7.808218555862453059, -4.508077085119343685, -7.999534413642745534 ) ) ;
#92399=ADVANCED_FACE ( 'NONE', ( #13737 ), #38136, .F. ) ;
#92475=LINE ( 'NONE', #84401, #56670 ) ;
#92488=CIRCLE ( 'NONE', #46005, 5.000000000000000000 ) ;
#92532=VECTOR ( 'NONE', #4046, 1000.000000000000000 ) ;
#92557=CIRCLE ( 'NONE', #42585, 5.000000000000000888 ) ;
#92606=CARTESIAN_POINT ( 'NONE',  ( -3.295171437451867469, -7.213553046160193993, -7.590212325761443779 ) ) ;
#92626=CARTESIAN_POINT ( 'NONE',  ( -5.276498195232381505, 6.073236878018020590, -7.633618187056802284 ) ) ;
#92627=CARTESIAN_POINT ( 'NONE',  ( -7.907996613752301229, -3.055722423191993276, -7.792112796859424151 ) ) ;
#92628=ADVANCED_FACE ( 'NONE', ( #33673 ), #33145, .F. ) ;
#92666=EDGE_CURVE ( 'NONE', #75037, #48423, #27749, .T. ) ;
#92689=CARTESIAN_POINT ( 'NONE',  ( -4.250000000000000000, 5.204748896376250699E-16, -8.028130060628445364 ) ) ;
#92691=ORIENTED_EDGE ( 'NONE', *, *, #101780, .T. ) ;
#92728=CARTESIAN_POINT ( 'NONE',  ( -7.500000000000000000, -4.330127018922201643, -7.422398894150036064 ) ) ;
#92754=AXIS2_PLACEMENT_3D ( 'NONE', #32798, #24184, #73210 ) ;
#92775=VECTOR ( 'NONE', #23209, 1000.000000000000000 ) ;
#92788=ORIENTED_EDGE ( 'NONE', *, *, #69682, .F. ) ;
#92827=LINE ( 'NONE', #75584, #100702 ) ;
#92988=CARTESIAN_POINT ( 'NONE',  ( 7.914973979435151463, 3.817460047930442357, -7.907502498112419786 ) ) ;
#93010=VERTEX_POINT ( 'NONE', #18975 ) ;
#93271=LINE ( 'NONE', #83566, #93746 ) ;
#93398=DIRECTION ( 'NONE',  ( 0.000000000000000000, 0.000000000000000000, 1.000000000000000000 ) ) ;
#93428=SURFACE_SIDE_STYLE ('',( #78812 ) ) ;
#93433=EDGE_CURVE ( 'NONE', #30487, #10075, #26112, .T. ) ;
#93518=CARTESIAN_POINT ( 'NONE',  ( 0.000000000000000000, 0.000000000000000000, -25.03750572909317285 ) ) ;
#93521=CARTESIAN_POINT ( 'NONE',  ( -7.500000000000000888, -3.608439182435170700, -7.298562697733109061 ) ) ;
#93616=CARTESIAN_POINT ( 'NONE',  ( 0.000000000000000000, 0.000000000000000000, -7.657127082228716297 ) ) ;
#93656=ORIENTED_EDGE ( 'NONE', *, *, #55813, .F. ) ;
#93675=AXIS2_PLACEMENT_3D ( 'NONE', #31101, #14326, #81704 ) ;
#93687=CARTESIAN_POINT ( 'NONE',  ( -0.3306966981845154141, -8.469326210127452015, -7.349897473154965333 ) ) ;
#93696=CARTESIAN_POINT ( 'NONE',  ( -7.808218555861020427, 4.508077085121809269, -7.999534413642737540 ) ) ;
#93734=EDGE_LOOP ( 'NONE', ( #87811, #55879, #101814, #48708 ) ) ;
#93740=DIRECTION ( 'NONE',  ( 0.000000000000000000, 0.000000000000000000, -1.000000000000000000 ) ) ;
#93746=VECTOR ( 'NONE', #11262, 1000.000000000000000 ) ;
#93799=DIRECTION ( 'NONE',  ( -1.000000000000000000, 0.000000000000000000, 0.000000000000000000 ) ) ;
#93823=CONICAL_SURFACE ( 'NONE', #47066, 4.250000000000000000, 0.9599310885968754814 ) ;
#93845=ORIENTED_EDGE ( 'NONE', *, *, #57170, .F. ) ;
#93867=CARTESIAN_POINT ( 'NONE',  ( 6.070808553813592639E-16, -8.895730773063899477, -7.917997657324742811 ) ) ;
#93918=CARTESIAN_POINT ( 'NONE',  ( 7.500000000000000000, -3.608439182435168924, -7.298562697733108173 ) ) ;
#94004=CONICAL_SURFACE ( 'NONE', #47487, 10.39117206796836257, 1.221730476396047926 ) ;
#94037=CARTESIAN_POINT ( 'NONE',  ( 6.249999999999997335, 5.051814855409223703, -7.198902722707428481 ) ) ;
#94061=DIRECTION ( 'NONE',  ( 0.000000000000000000, 0.000000000000000000, 1.000000000000000000 ) ) ;
#94066=CARTESIAN_POINT ( 'NONE',  ( -4.250000000000000000, 5.204748896376250699E-16, -1.971869939371574620 ) ) ;
#94119=DIRECTION ( 'NONE',  ( -0.000000000000000000, -0.000000000000000000, -1.000000000000000000 ) ) ;
#94133=CARTESIAN_POINT ( 'NONE',  ( 10.12668159690567649, 0.000000000000000000, -10.00000000000000000 ) ) ;
#94174=ORIENTED_EDGE ( 'NONE', *, *, #78052, .F. ) ;
#94227=CARTESIAN_POINT ( 'NONE',  ( -7.549004593702460575, 4.358419834287831307, -7.700121441565837443 ) ) ;
#94271=VERTEX_POINT ( 'NONE', #77732 ) ;
#94324=CARTESIAN_POINT ( 'NONE',  ( 0.5984201754795559491, 8.314755988442765755, -0.7022220667781327030 ) ) ;
#94339=CARTESIAN_POINT ( 'NONE',  ( 0.000000000000000000, 0.000000000000000000, -4.289342857142857568 ) ) ;
#94350=FACE_OUTER_BOUND ( 'NONE', #39597, .T. ) ;
#94351=ORIENTED_EDGE ( 'NONE', *, *, #95120, .F. ) ;
#94374=CARTESIAN_POINT ( 'NONE',  ( 4.250000000000000000, 0.000000000000000000, -3.393184225085859929 ) ) ;
#94397=CARTESIAN_POINT ( 'NONE',  ( -5.000000000000000000, 0.000000000000000000, -9.974599999999998801 ) ) ;
#94412=DIRECTION ( 'NONE',  ( 0.000000000000000000, 0.000000000000000000, -1.000000000000000000 ) ) ;
#94450=AXIS2_PLACEMENT_3D ( 'NONE', #79370, #38927, #62676 ) ;
#94514=EDGE_LOOP ( 'NONE', ( #101103, #79324, #60478, #27987 ) ) ;
#94555=EDGE_LOOP ( 'NONE', ( #65465, #66109, #70133, #87169, #12999 ) ) ;
#94571=ADVANCED_FACE ( 'NONE', ( #32122 ), #106513, .F. ) ;
#94773=CARTESIAN_POINT ( 'NONE',  ( -7.922281120364393914, 4.573931137438267847, -8.047472243342932430 ) ) ;
#94781=DIRECTION ( 'NONE',  ( -0.000000000000000000, -0.000000000000000000, 1.000000000000000000 ) ) ;
#94791=CARTESIAN_POINT ( 'NONE',  ( 0.000000000000000000, 0.000000000000000000, -1.971869939371574620 ) ) ;
#94808=DIRECTION ( 'NONE',  ( -0.000000000000000000, -0.000000000000000000, -1.000000000000000000 ) ) ;
#94818=FACE_OUTER_BOUND ( 'NONE', #12307, .T. ) ;
#94830=EDGE_CURVE ( 'NONE', #4153, #106581, #100441, .T. ) ;
#94862=CARTESIAN_POINT ( 'NONE',  ( 3.093157300003886334, 6.874418838041290059, 2.297153352953662914E-15 ) ) ;
#94870=CARTESIAN_POINT ( 'NONE',  ( 0.000000000000000000, 0.000000000000000000, -0.02540000000000007530 ) ) ;
#94907=EDGE_CURVE ( 'NONE', #91741, #62962, #62575, .T. ) ;
#95030=( NAMED_UNIT ( * ) PLANE_ANGLE_UNIT ( ) SI_UNIT ( $, .RADIAN. ) );
#95099=EDGE_CURVE ( 'NONE', #95526, #64087, #38245, .T. ) ;
#95120=EDGE_CURVE ( 'NONE', #11929, #62962, #16587, .T. ) ;
#95218=ORIENTED_EDGE ( 'NONE', *, *, #59964, .T. ) ;
#95241=ORIENTED_EDGE ( 'NONE', *, *, #103491, .T. ) ;
#95245=CARTESIAN_POINT ( 'NONE',  ( 7.500000000000000888, -3.988190556646206364, -0.8526458641284285767 ) ) ;
#95275=CARTESIAN_POINT ( 'NONE',  ( 0.000000000000000000, 0.000000000000000000, -10.00000000000000000 ) ) ;
#95366=STYLED_ITEM ( 'NONE', ( #62658 ), #44833 ) ;
#95369=ORIENTED_EDGE ( 'NONE', *, *, #91017, .F. ) ;
#95432=CARTESIAN_POINT ( 'NONE',  ( 1.060314165523193353, 8.048081368953958759, -7.659344964962508051 ) ) ;
#95526=VERTEX_POINT ( 'NONE', #12467 ) ;
#95546=DIRECTION ( 'NONE',  ( -0.000000000000000000, -0.000000000000000000, -1.000000000000000000 ) ) ;
#95550=AXIS2_PLACEMENT_3D ( 'NONE', #53001, #3386, #17987 ) ;
#95568=ADVANCED_FACE ( 'NONE', ( #27658, #43788 ), #53483, .F. ) ;
#95584=CARTESIAN_POINT ( 'NONE',  ( 4.250000000000000000, 0.000000000000000000, -7.657127082228716297 ) ) ;
#95632=DIRECTION ( 'NONE',  ( -0.000000000000000000, -0.000000000000000000, 1.000000000000000000 ) ) ;
#95910=ORIENTED_EDGE ( 'NONE', *, *, #62587, .T. ) ;
#95919=DIRECTION ( 'NONE',  ( -0.000000000000000000, -0.000000000000000000, -1.000000000000000000 ) ) ;
#95945=EDGE_LOOP ( 'NONE', ( #60848, #14458, #548, #9990, #14675 ) ) ;
#95955=CARTESIAN_POINT ( 'NONE',  ( 3.096526599377916078, -6.872473572140724407, -6.510295232596552406E-15 ) ) ;
#95957=CARTESIAN_POINT ( 'NONE',  ( 4.174999999999998934, 0.000000000000000000, -0.5776712190230098853 ) ) ;
#96066=VECTOR ( 'NONE', #15528, 1000.000000000000000 ) ;
#96086=CARTESIAN_POINT ( 'NONE',  ( 5.000000000000000000, 6.123233995736766282E-16, -8.553285714285713937 ) ) ;
#96089=CARTESIAN_POINT ( 'NONE',  ( 7.500000000000000000, -3.157198044629119682, -7.642795354506497496 ) ) ;
#96132=ORIENTED_EDGE ( 'NONE', *, *, #84912, .F. ) ;
#96150=CARTESIAN_POINT ( 'NONE',  ( -4.250000000000000000, 5.204748896376250699E-16, -0.5505556536572887572 ) ) ;
#96237=EDGE_CURVE ( 'NONE', #35664, #90336, #46919, .T. ) ;
#96318=VERTEX_POINT ( 'NONE', #69812 ) ;
#96325=CARTESIAN_POINT ( 'NONE',  ( 0.000000000000000000, 0.000000000000000000, -8.500000000000000000 ) ) ;
#96332=DIRECTION ( 'NONE',  ( -0.000000000000000000, -0.000000000000000000, -1.000000000000000000 ) ) ;
#96349=DIRECTION ( 'NONE',  ( 0.000000000000000000, 0.000000000000000000, 1.000000000000000000 ) ) ;
#96447=FACE_OUTER_BOUND ( 'NONE', #10247, .T. ) ;
#96453=EDGE_CURVE ( 'NONE', #64087, #106581, #100311, .T. ) ;
#96461=CARTESIAN_POINT ( 'NONE',  ( -5.000000000000000000, 0.000000000000000000, -5.710657142857142432 ) ) ;
#96524=DIRECTION ( 'NONE',  ( 0.000000000000000000, 0.000000000000000000, 1.000000000000000000 ) ) ;
#96554=EDGE_CURVE ( 'NONE', #69179, #22401, #13415, .T. ) ;
#96681=EDGE_LOOP ( 'NONE', ( #104118, #66469, #67919 ) ) ;
#96726=ORIENTED_EDGE ( 'NONE', *, *, #99922, .F. ) ;
#96785=ORIENTED_EDGE ( 'NONE', *, *, #84078, .F. ) ;
#96828=CARTESIAN_POINT ( 'NONE',  ( -7.500000000000000000, 1.854554393013820190, -0.1880126015361690550 ) ) ;
#96921=VERTEX_POINT ( 'NONE', #32653 ) ;
#96959=CARTESIAN_POINT ( 'NONE',  ( 0.000000000000000000, 0.000000000000000000, -0.02540000000000007530 ) ) ;
#97001=CARTESIAN_POINT ( 'NONE',  ( -0.5974722283283669944, 8.315303285985685022, -0.7026937717022826435 ) ) ;
#97092=ORIENTED_EDGE ( 'NONE', *, *, #43266, .T. ) ;
#97132=CARTESIAN_POINT ( 'NONE',  ( 7.915340744421998309, 3.857466640755272902, -7.913699667209542987 ) ) ;
#97150=EDGE_CURVE ( 'NONE', #10693, #20907, #71492, .T. ) ;
#97157=EDGE_CURVE ( 'NONE', #48423, #75037, #43684, .T. ) ;
#97235=CIRCLE ( 'NONE', #69690, 5.000000000000000000 ) ;
#97316=CARTESIAN_POINT ( 'NONE',  ( 5.088535779738191600, -5.722386535631965643, -7.491772860716527482 ) ) ;
#97498=ADVANCED_FACE ( 'NONE', ( #53852 ), #31706, .F. ) ;
#97502=CARTESIAN_POINT ( 'NONE',  ( 4.250000000000000000, 0.000000000000000000, -10.00000000000000000 ) ) ;
#97503=CARTESIAN_POINT ( 'NONE',  ( 4.250000000000000000, 0.000000000000000000, -4.814498510800145681 ) ) ;
#97532=AXIS2_PLACEMENT_3D ( 'NONE', #21659, #37852, #70715 ) ;
#97625=ORIENTED_EDGE ( 'NONE', *, *, #6584, .F. ) ;
#97847=DIRECTION ( 'NONE',  ( -0.000000000000000000, -0.000000000000000000, -1.000000000000000000 ) ) ;
#97849=CARTESIAN_POINT ( 'NONE',  ( 0.9763930676201736381, -8.096533237419009765, -7.213065638942138591 ) ) ;
#97852=CARTESIAN_POINT ( 'NONE',  ( -7.500000000000667910, 3.157052757786715791, -7.642767288268637493 ) ) ;
#97871=CARTESIAN_POINT ( 'NONE',  ( -7.499999999999998224, 1.489914625144000082, -0.1187923833806731472 ) ) ;
#97879=DIRECTION ( 'NONE',  ( -1.000000000000000000, 0.000000000000000000, 0.000000000000000000 ) ) ;
#97885=CARTESIAN_POINT ( 'NONE',  ( 0.000000000000000000, 0.000000000000000000, -0.5776712190230098853 ) ) ;
#97908=SURFACE_SIDE_STYLE ('',( #106525 ) ) ;
#97989=DIRECTION ( 'NONE',  ( -0.000000000000000000, -0.000000000000000000, 1.000000000000000000 ) ) ;
#98072=CARTESIAN_POINT ( 'NONE',  ( 7.549006887134069643, -4.358421158401203144, -7.700127545397313256 ) ) ;
#98092=AXIS2_PLACEMENT_3D ( 'NONE', #34754, #34218, #58464 ) ;
#98155=ADVANCED_FACE ( 'NONE', ( #1727 ), #26595, .F. ) ;
#98246=ORIENTED_EDGE ( 'NONE', *, *, #84912, .T. ) ;
#98272=ORIENTED_EDGE ( 'NONE', *, *, #104253, .F. ) ;
#98427=CARTESIAN_POINT ( 'NONE',  ( 0.000000000000000000, 0.000000000000000000, 0.000000000000000000 ) ) ;
#98451=FACE_OUTER_BOUND ( 'NONE', #41753, .T. ) ;
#98512=UNCERTAINTY_MEASURE_WITH_UNIT (LENGTH_MEASURE( 1.000000000000000082E-05 ), #44885, 'distance_accuracy_value', 'NONE');
#98553=ADVANCED_FACE ( 'NONE', ( #41535 ), #99773, .F. ) ;
#98567=VECTOR ( 'NONE', #94781, 1000.000000000000000 ) ;
#98680=CARTESIAN_POINT ( 'NONE',  ( -3.749999999999998224, -6.495190528383299799, -6.991905250253757309 ) ) ;
#98684=CARTESIAN_POINT ( 'NONE',  ( 7.894787914004607998, -0.7647108141804129788, -7.591390474663422872 ) ) ;
#98707=CARTESIAN_POINT ( 'NONE',  ( -0.6511518506208961998, 8.763486134561265573, -7.907570769506046204 ) ) ;
#98745=CARTESIAN_POINT ( 'NONE',  ( 4.250000000000000000, 0.000000000000000000, -10.00000000000000000 ) ) ;
#98967=CARTESIAN_POINT ( 'NONE',  ( 1.250000000000000444, -7.938566201357371455, -7.198902722707432922 ) ) ;
#98971=VECTOR ( 'NONE', #38736, 1000.000000000000000 ) ;
#98978=PRODUCT_DEFINITION ( 'UNKNOWN', '', #47295, #43483 ) ;
#99135=EDGE_LOOP ( 'NONE', ( #67847, #22952, #34846 ) ) ;
#99213=CARTESIAN_POINT ( 'NONE',  ( -4.999999999999999112, -5.773502691896267969, -7.063244554130005071 ) ) ;
#99329=ORIENTED_EDGE ( 'NONE', *, *, #100030, .T. ) ;
#99353=B_SPLINE_CURVE_WITH_KNOTS ( 'NONE', 3,
 ( #51783, #26501, #74459, #10780, #84696, #51240, #43699, #76058, #17319, #9189 ),
 .UNSPECIFIED., .F., .F.,
 ( 4, 2, 2, 2, 4 ),
 ( 0.000000000000000000, 0.002305503304226492068, 0.004611006608452984136, 0.006916509912679475770, 0.009222013216905964803 ),
 .UNSPECIFIED. ) ;
#99426=FACE_OUTER_BOUND ( 'NONE', #17723, .T. ) ;
#99446=CARTESIAN_POINT ( 'NONE',  ( 1.306442393143576908, 8.377108146505385378, -7.792327460285857654 ) ) ;
#99468=DIRECTION ( 'NONE',  ( 1.000000000000000000, 0.000000000000000000, 0.000000000000000000 ) ) ;
#99501=DIRECTION ( 'NONE',  ( -1.000000000000000000, 0.000000000000000000, 0.000000000000000000 ) ) ;
#99512=B_SPLINE_CURVE_WITH_KNOTS ( 'NONE', 3,
 ( #63941, #46670, #73044, #97871, #96828, #24027, #48774, #29987, #104367, #70952 ),
 .UNSPECIFIED., .F., .F.,
 ( 4, 2, 2, 2, 4 ),
 ( 0.01051144076094937159, 0.01162027323572613000, 0.01272910571050288667, 0.01383793818527964507, 0.01494677066005640348 ),
 .UNSPECIFIED. ) ;
#99583=DIRECTION ( 'NONE',  ( -1.000000000000000000, 0.000000000000000000, 0.000000000000000000 ) ) ;
#99712=ORIENTED_EDGE ( 'NONE', *, *, #26387, .T. ) ;
#99772=CARTESIAN_POINT ( 'NONE',  ( 4.250000000000000000, 0.000000000000000000, -10.00000000000000000 ) ) ;
#99773=CYLINDRICAL_SURFACE ( 'NONE', #78323, 4.250000000000000000 ) ;
#99788=CARTESIAN_POINT ( 'NONE',  ( -6.601567268551446155, 5.319966374295964862, -7.792327460285857654 ) ) ;
#99790=ORIENTED_EDGE ( 'NONE', *, *, #79227, .F. ) ;
#99811=AXIS2_PLACEMENT_3D ( 'NONE', #14437, #95919, #23107 ) ;
#99922=EDGE_CURVE ( 'NONE', #52946, #57728, #83625, .T. ) ;
#99923=AXIS2_PLACEMENT_3D ( 'NONE', #81781, #97989, #23067 ) ;
#99934=DIRECTION ( 'NONE',  ( -1.000000000000000000, 0.000000000000000000, 0.000000000000000000 ) ) ;
#99948=AXIS2_PLACEMENT_3D ( 'NONE', #55584, #95546, #88522 ) ;
#99991=CARTESIAN_POINT ( 'NONE',  ( 0.6508621380849222149, 8.763657152406448603, -7.907633014911220393 ) ) ;
#100030=EDGE_CURVE ( 'NONE', #44884, #59052, #84087, .T. ) ;
#100039=LINE ( 'NONE', #59065, #3351 ) ;
#100041=CARTESIAN_POINT ( 'NONE',  ( -4.250000000000000000, 5.204748896376250699E-16, -10.00000000000000000 ) ) ;
#100141=DIRECTION ( 'NONE',  ( -0.000000000000000000, -0.000000000000000000, -1.000000000000000000 ) ) ;
#100180=CARTESIAN_POINT ( 'NONE',  ( 7.500000000000000000, 4.330127018922189208, -7.422398894150033399 ) ) ;
#100189=DIRECTION ( 'NONE',  ( 0.000000000000000000, 0.000000000000000000, 1.000000000000000000 ) ) ;
#100195=DIRECTION ( 'NONE',  ( 1.000000000000000000, 0.000000000000000000, 0.000000000000000000 ) ) ;
#100286=CARTESIAN_POINT ( 'NONE',  ( -0.6250000000000013323, -8.299410119600887370, -7.298562697733112614 ) ) ;
#100290=EDGE_CURVE ( 'NONE', #34186, #91741, #28794, .T. ) ;
#100311=LINE ( 'NONE', #59345, #3978 ) ;
#100339=APPLICATION_CONTEXT ( 'automotive_design' ) ;
#100363=ORIENTED_EDGE ( 'NONE', *, *, #77851, .T. ) ;
#100365=VERTEX_POINT ( 'NONE', #28253 ) ;
#100441=CIRCLE ( 'NONE', #33337, 5.000000000000000000 ) ;
#100446=DIRECTION ( 'NONE',  ( -0.000000000000000000, -0.000000000000000000, -1.000000000000000000 ) ) ;
#100464=LINE ( 'NONE', #90796, #37532 ) ;
#100467=VECTOR ( 'NONE', #77659, 1000.000000000000000 ) ;
#100474=ORIENTED_EDGE ( 'NONE', *, *, #6941, .T. ) ;
#100490=ORIENTED_EDGE ( 'NONE', *, *, #91017, .T. ) ;
#100509=CARTESIAN_POINT ( 'NONE',  ( 4.406842699996129653, -6.115962218725295330, -6.735605996566196296E-15 ) ) ;
#100537=ORIENTED_EDGE ( 'NONE', *, *, #97157, .T. ) ;
#100596=B_SPLINE_CURVE_WITH_KNOTS ( 'NONE', 3,
 ( #82821, #25699, #32160, #83347, #106015, #8919, #49372, #32706 ),
 .UNSPECIFIED., .F., .F.,
 ( 4, 2, 2, 4 ),
 ( 0.006061689441712471600, 0.007174127271521696381, 0.008286565101330922029, 0.01051144076094937159 ),
 .UNSPECIFIED. ) ;
#100648=ORIENTED_EDGE ( 'NONE', *, *, #100290, .T. ) ;
#100702=VECTOR ( 'NONE', #101463, 1000.000000000000000 ) ;
#100844=EDGE_CURVE ( 'NONE', #11929, #103169, #76947, .T. ) ;
#100897=ORIENTED_EDGE ( 'NONE', *, *, #101333, .F. ) ;
#100915=B_SPLINE_CURVE_WITH_KNOTS ( 'NONE', 3,
 ( #92728, #67410, #74409, #99213, #98680, #24834, #8619, #100286, #75480 ),
 .UNSPECIFIED., .F., .F.,
 ( 4, 2, 1, 2, 4 ),
 ( 0.000000000000000000, 0.002165063509461097498, 0.004330127018922194995, 0.006495190528383292493, 0.008660254037844389990 ),
 .UNSPECIFIED. ) ;
#100953=CARTESIAN_POINT ( 'NONE',  ( -4.250000000000000000, 5.204748896376250699E-16, -0.9215586320570148260 ) ) ;
#101103=ORIENTED_EDGE ( 'NONE', *, *, #33139, .F. ) ;
#101150=AXIS2_PLACEMENT_3D ( 'NONE', #15571, #8004, #40914 ) ;
#101164=AXIS2_PLACEMENT_3D ( 'NONE', #77402, #3518, #20281 ) ;
#101215=DIRECTION ( 'NONE',  ( 1.000000000000000000, 0.000000000000000000, 0.000000000000000000 ) ) ;
#101245=CARTESIAN_POINT ( 'NONE',  ( 4.250000000000000000, 0.000000000000000000, -0.5505556536572887572 ) ) ;
#101266=CARTESIAN_POINT ( 'NONE',  ( -4.599534470795829222, 6.460478697738384568, -7.590212325761545031 ) ) ;
#101268=CARTESIAN_POINT ( 'NONE',  ( -7.897836333153806621, -1.530409084195007985, -7.633857274177629826 ) ) ;
#101296=FACE_OUTER_BOUND ( 'NONE', #93734, .T. ) ;
#101308=DIRECTION ( 'NONE',  ( 0.000000000000000000, 0.000000000000000000, 1.000000000000000000 ) ) ;
#101325=ORIENTED_EDGE ( 'NONE', *, *, #20690, .F. ) ;
#101333=EDGE_CURVE ( 'NONE', #100365, #90212, #4667, .T. ) ;
#101372=CARTESIAN_POINT ( 'NONE',  ( 0.000000000000000000, 0.000000000000000000, 1.734723475976807094E-15 ) ) ;
#101398=EDGE_LOOP ( 'NONE', ( #1239, #36201, #103339, #27448 ) ) ;
#101463=DIRECTION ( 'NONE',  ( -0.8191520442889924647, 1.003171929053525486E-16, 0.5735764363510451602 ) ) ;
#101522=CIRCLE ( 'NONE', #68818, 7.500000000000003553 ) ;
#101542=DIRECTION ( 'NONE',  ( -0.000000000000000000, -0.000000000000000000, -1.000000000000000000 ) ) ;
#101601=FACE_OUTER_BOUND ( 'NONE', #83956, .T. ) ;
#101670=CARTESIAN_POINT ( 'NONE',  ( -1.908195823574487804E-14, -8.660254037844390851, -0.9999999999999974465 ) ) ;
#101738=LINE ( 'NONE', #19809, #19904 ) ;
#101780=EDGE_CURVE ( 'NONE', #55329, #57292, #92488, .T. ) ;
#101781=EDGE_CURVE ( 'NONE', #18381, #59052, #79461, .T. ) ;
#101814=ORIENTED_EDGE ( 'NONE', *, *, #49242, .F. ) ;
#101913=DIRECTION ( 'NONE',  ( 0.8191520442889884679, 0.000000000000000000, 0.5735764363510508224 ) ) ;
#101960=DIRECTION ( 'NONE',  ( 1.000000000000000000, 0.000000000000000000, 0.000000000000000000 ) ) ;
#101977=EDGE_CURVE ( 'NONE', #82359, #9383, #102973, .T. ) ;
#101984=CARTESIAN_POINT ( 'NONE',  ( -7.500000000000000000, -4.330127018922201643, -10.00000000000000000 ) ) ;
#101985=EDGE_CURVE ( 'NONE', #62254, #77573, #20346, .T. ) ;
#102085=ORIENTED_EDGE ( 'NONE', *, *, #56141, .F. ) ;
#102207=ORIENTED_EDGE ( 'NONE', *, *, #48393, .T. ) ;
#102213=VECTOR ( 'NONE', #73751, 1000.000000000000000 ) ;
#102222=LINE ( 'NONE', #19763, #20626 ) ;
#102267=ORIENTED_EDGE ( 'NONE', *, *, #41286, .T. ) ;
#102453=LINE ( 'NONE', #94374, #67289 ) ;
#102528=DIRECTION ( 'NONE',  ( 0.000000000000000000, 0.000000000000000000, 1.000000000000000000 ) ) ;
#102548=FACE_OUTER_BOUND ( 'NONE', #17001, .T. ) ;
#102589=CARTESIAN_POINT ( 'NONE',  ( 7.500000000000000000, -3.202733125952014426, -7.213074474936427727 ) ) ;
#102612=ADVANCED_FACE ( 'NONE', ( #84889 ), #77861, .F. ) ;
#102615=DIRECTION ( 'NONE',  ( -0.000000000000000000, -0.000000000000000000, -1.000000000000000000 ) ) ;
#102659=CARTESIAN_POINT ( 'NONE',  ( -10.39117206796836435, 1.272551561242683961E-15, -8.500000000000000000 ) ) ;
#102664=CARTESIAN_POINT ( 'NONE',  ( -7.499999999999999112, 1.443375672974058110, -7.063244554130000630 ) ) ;
#102665=ORIENTED_EDGE ( 'NONE', *, *, #57170, .T. ) ;
#102892=ORIENTED_EDGE ( 'NONE', *, *, #94830, .T. ) ;
#102937=CARTESIAN_POINT ( 'NONE',  ( 2.452879891156805936, 7.244083172395182402, -0.1007566405101772145 ) ) ;
#102973=CIRCLE ( 'NONE', #59873, 10.39117206796836257 ) ;
#103079=EDGE_CURVE ( 'NONE', #96318, #90212, #86, .T. ) ;
#103104=DIRECTION ( 'NONE',  ( -0.8191520442889884679, 1.003171929053520679E-16, 0.5735764363510508224 ) ) ;
#103122=CARTESIAN_POINT ( 'NONE',  ( 7.500000000000000888, -4.651016565836964212, -7.928861822685564498 ) ) ;
#103146=DIRECTION ( 'NONE',  ( -0.000000000000000000, -0.000000000000000000, -1.000000000000000000 ) ) ;
#103164=ADVANCED_FACE ( 'NONE', ( #96447 ), #31720, .F. ) ;
#103169=VERTEX_POINT ( 'NONE', #14965 ) ;
#103178=CARTESIAN_POINT ( 'NONE',  ( 0.000000000000000000, 0.000000000000000000, -2.868028571428571372 ) ) ;
#103196=DIRECTION ( 'NONE',  ( 1.000000000000000000, 0.000000000000000000, 0.000000000000000000 ) ) ;
#103220=CARTESIAN_POINT ( 'NONE',  ( 0.000000000000000000, 0.000000000000000000, -7.131971428571428184 ) ) ;
#103335=ORIENTED_EDGE ( 'NONE', *, *, #31292, .F. ) ;
#103336=EDGE_CURVE ( 'NONE', #9383, #82359, #44892, .T. ) ;
#103339=ORIENTED_EDGE ( 'NONE', *, *, #1960, .T. ) ;
#103367=AXIS2_PLACEMENT_3D ( 'NONE', #65955, #100446, #90770 ) ;
#103467=FACE_OUTER_BOUND ( 'NONE', #80966, .T. ) ;
#103491=EDGE_CURVE ( 'NONE', #62254, #23008, #67791, .T. ) ;
#103519=ORIENTED_EDGE ( 'NONE', *, *, #65240, .F. ) ;
#103521=CARTESIAN_POINT ( 'NONE',  ( 2.387978478800936610, 7.281554020289634721, -7.069802615102036114 ) ) ;
#103549=CARTESIAN_POINT ( 'NONE',  ( 0.000000000000000000, 0.000000000000000000, -7.131971428571428184 ) ) ;
#103682=B_SPLINE_CURVE_WITH_KNOTS ( 'NONE', 3,
 ( #17691, #26878, #92627, #101268, #18785, #34438 ),
 .UNSPECIFIED., .F., .F.,
 ( 4, 2, 4 ),
 ( 0.000000000000000000, 0.002307655110370377804, 0.004615310220740755608 ),
 .UNSPECIFIED. ) ;
#103747=ADVANCED_FACE ( 'NONE', ( #47742 ), #27753, .F. ) ;
#103762=FACE_OUTER_BOUND ( 'NONE', #24186, .T. ) ;
#103782=FACE_OUTER_BOUND ( 'NONE', #53634, .T. ) ;
#103804=CARTESIAN_POINT ( 'NONE',  ( -3.750000000000004441, -6.495190528383288253, 1.734723475976807094E-15 ) ) ;
#103851=EDGE_CURVE ( 'NONE', #37257, #14360, #48461, .T. ) ;
#103931=CARTESIAN_POINT ( 'NONE',  ( 4.250000000000000000, 0.000000000000000000, -3.393184225085859929 ) ) ;
#103983=CARTESIAN_POINT ( 'NONE',  ( 0.000000000000000000, 8.660254037844390851, -0.9999999999999974465 ) ) ;
#103989=CARTESIAN_POINT ( 'NONE',  ( 7.808623696107298784, 4.508310992947659024, -7.999704684617482187 ) ) ;
#104007=ORIENTED_EDGE ( 'NONE', *, *, #9325, .T. ) ;
#104033=ORIENTED_EDGE ( 'NONE', *, *, #31292, .T. ) ;
#104044=CARTESIAN_POINT ( 'NONE',  ( 5.174575781541514097, 5.672711317429273592, -7.030005583190789942 ) ) ;
#104072=CARTESIAN_POINT ( 'NONE',  ( 3.750000000000004885, -6.495190528383287365, 1.734723475976807094E-15 ) ) ;
#104118=ORIENTED_EDGE ( 'NONE', *, *, #103851, .T. ) ;
#104165=CARTESIAN_POINT ( 'NONE',  ( 7.908230272949222872, -3.123266379892265299, -7.776722524729861696 ) ) ;
#104253=EDGE_CURVE ( 'NONE', #20962, #13350, #57083, .T. ) ;
#104294=DIRECTION ( 'NONE',  ( -0.000000000000000000, -0.000000000000000000, 1.000000000000000000 ) ) ;
#104304=CARTESIAN_POINT ( 'NONE',  ( 5.000000000000000000, 6.123233995736766282E-16, -1.446714285714285841 ) ) ;
#104354=VERTEX_POINT ( 'NONE', #73786 ) ;
#104367=CARTESIAN_POINT ( 'NONE',  ( -7.500000000000000888, 3.988838049906422434, -0.8529248949437571170 ) ) ;
#104408=PRESENTATION_STYLE_ASSIGNMENT (( #40205 ) ) ;
#104550=FACE_OUTER_BOUND ( 'NONE', #51607, .T. ) ;
#104556=CARTESIAN_POINT ( 'NONE',  ( -1.249327701954737080, 8.410337540188283612, -7.776713651267457728 ) ) ;
#104590=VERTEX_POINT ( 'NONE', #101670 ) ;
#104591=ORIENTED_EDGE ( 'NONE', *, *, #2572, .F. ) ;
#104723=DIRECTION ( 'NONE',  ( -1.000000000000000000, 0.000000000000000000, 0.000000000000000000 ) ) ;
#104787=DIRECTION ( 'NONE',  ( -1.000000000000000000, 0.000000000000000000, 0.000000000000000000 ) ) ;
#104826=DIRECTION ( 'NONE',  ( 0.000000000000000000, 0.000000000000000000, 1.000000000000000000 ) ) ;
#104852=VECTOR ( 'NONE', #80781, 1000.000000000000000 ) ;
#104877=CARTESIAN_POINT ( 'NONE',  ( -0.5984201754795734907, -8.314755988442767531, -0.7022220667781350345 ) ) ;
#104900=ADVANCED_FACE ( 'NONE', ( #67058 ), #70812, .F. ) ;
#105035=ORIENTED_EDGE ( 'NONE', *, *, #92073, .T. ) ;
#105063=ORIENTED_EDGE ( 'NONE', *, *, #4678, .T. ) ;
#105121=CARTESIAN_POINT ( 'NONE',  ( -0.2791032213812740803, 8.821394357840562250, -7.929128246061908136 ) ) ;
#105171=AXIS2_PLACEMENT_3D ( 'NONE', #201, #66037, #33165 ) ;
#105175=DIRECTION ( 'NONE',  ( -1.000000000000000000, 0.000000000000000000, 0.000000000000000000 ) ) ;
#105301=DIRECTION ( 'NONE',  ( 0.8191520442889913545, 1.003171929053524254E-16, -0.5735764363510468256 ) ) ;
#105343=LINE ( 'NONE', #31488, #37687 ) ;
#105350=EDGE_CURVE ( 'NONE', #62254, #4153, #41574, .T. ) ;
#105374=DIRECTION ( 'NONE',  ( 1.000000000000000000, 0.000000000000000000, 0.000000000000000000 ) ) ;
#105406=ORIENTED_EDGE ( 'NONE', *, *, #87345, .T. ) ;
#105408=CARTESIAN_POINT ( 'NONE',  ( 5.000000000000000888, 0.000000000000000000, -10.00000000000000000 ) ) ;
#105417=CARTESIAN_POINT ( 'NONE',  ( 0.000000000000000000, 0.000000000000000000, -1.446714285714285841 ) ) ;
#105424=CARTESIAN_POINT ( 'NONE',  ( -7.922811899608408481, -4.628803996615327598, -8.057669882367651581 ) ) ;
#105464=DIRECTION ( 'NONE',  ( -1.000000000000000000, 0.000000000000000000, 0.000000000000000000 ) ) ;
#105526=CARTESIAN_POINT ( 'NONE',  ( 4.250000000000000000, 0.000000000000000000, -1.971869939371574620 ) ) ;
#105705=AXIS2_PLACEMENT_3D ( 'NONE', #55852, #38154, #86695 ) ;
#105724=CARTESIAN_POINT ( 'NONE',  ( 7.908030677224555660, -3.059924800338351236, -7.792662696733370531 ) ) ;
#105785=EDGE_CURVE ( 'NONE', #104590, #14360, #56440, .T. ) ;
#105852=EDGE_LOOP ( 'NONE', ( #102267, #91572, #45273, #102085 ) ) ;
#106015=CARTESIAN_POINT ( 'NONE',  ( -7.500000000000000000, -2.571118828324945760, -0.3627527587569074896 ) ) ;
#106136=DIRECTION ( 'NONE',  ( 0.8191520442889924647, 0.000000000000000000, 0.5735764363510451602 ) ) ;
#106193=DIRECTION ( 'NONE',  ( -1.000000000000000000, 0.000000000000000000, 0.000000000000000000 ) ) ;
#106311=VERTEX_POINT ( 'NONE', #91233 ) ;
#106395=CARTESIAN_POINT ( 'NONE',  ( -2.352990130084491319E-16, 8.660254037844390851, -7.422398894150036064 ) ) ;
#106407=ORIENTED_EDGE ( 'NONE', *, *, #101985, .T. ) ;
#106416=DIRECTION ( 'NONE',  ( 0.000000000000000000, 0.000000000000000000, 1.000000000000000000 ) ) ;
#106431=ORIENTED_EDGE ( 'NONE', *, *, #4837, .F. ) ;
#106467=CARTESIAN_POINT ( 'NONE',  ( 5.000000000000000000, 6.123233995736766282E-16, -5.710657142857142432 ) ) ;
#106476=CIRCLE ( 'NONE', #35937, 4.250000000000000000 ) ;
#106482=APPLICATION_CONTEXT ( 'automotive_design' ) ;
#106513=CYLINDRICAL_SURFACE ( 'NONE', #9115, 4.250000000000000000 ) ;
#106525=SURFACE_STYLE_FILL_AREA ( #32139 ) ;
#106581=VERTEX_POINT ( 'NONE', #82994 ) ;
#106706=FACE_OUTER_BOUND ( 'NONE', #9950, .T. ) ;
#106747=DIRECTION ( 'NONE',  ( 1.000000000000000000, 0.000000000000000000, 0.000000000000000000 ) ) ;
ENDSEC;
END-ISO-10303-21;
